ISO-10303-21;
HEADER;
FILE_DESCRIPTION (('STEP AP214'),
    '1' );
FILE_NAME ('MAT-019 Puller.step',
    '2026-10-23T20:35:44',
    ( '' ),
    ( '' ),
    'SwSTEP 2.0',
    'SolidWorks 2025',
    '' );
FILE_SCHEMA (( 'AUTOMOTIVE_DESIGN' ));
ENDSEC;

DATA;
#8=CARTESIAN_POINT ( 'NONE',  ( -1.023371766162646468, 0.4368380215374090825, -1.573834103987475475 ) ) ;
#9=ADVANCED_FACE ( 'NONE', ( #4327 ), #5594, .T. ) ;
#16=CARTESIAN_POINT ( 'NONE',  ( -0.4330708661417322913, -0.9666437042230143772, -1.454455828411337359 ) ) ;
#26=TOROIDAL_SURFACE ( 'NONE', #1116, 1.223643328182681289, 0.05905511811023622659 ) ;
#27=DIRECTION ( 'NONE',  ( -0.000000000000000000, 1.000000000000000000, 0.000000000000000000 ) ) ;
#33=CARTESIAN_POINT ( 'NONE',  ( -0.4330708661417322913, 0.9666437042230143772, -1.454455828411337359 ) ) ;
#35=CIRCLE ( 'NONE', #6758, 1.377952755905511806 ) ;
#36=CARTESIAN_POINT ( 'NONE',  ( -0.4330708661417317917, -1.051607547633158557, -1.573502280244650997 ) ) ;
#42=CARTESIAN_POINT ( 'NONE',  ( 0.4637694296357178780, 0.9984400756355444884, -1.410742812766313969 ) ) ;
#44=ORIENTED_EDGE ( 'NONE', *, *, #3935, .F. ) ;
#47=CARTESIAN_POINT ( 'NONE',  ( -4.923936545553797639E-15, 0.4700904924197870649, -2.204724409448822975 ) ) ;
#53=TOROIDAL_SURFACE ( 'NONE', #1389, 1.223643328182681289, 0.05905511811023622659 ) ;
#54=CARTESIAN_POINT ( 'NONE',  ( -1.051607547633157225, -0.4330708661417354555, -1.573502280244651441 ) ) ;
#56=ORIENTED_EDGE ( 'NONE', *, *, #571, .F. ) ;
#58=CARTESIAN_POINT ( 'NONE',  ( 0.9346848099469073912, -0.4388997119412443304, -1.455943619906241215 ) ) ;
#59=CARTESIAN_POINT ( 'NONE',  ( 0.000000000000000000, 0.000000000000000000, -1.515748031496062964 ) ) ;
#65=CARTESIAN_POINT ( 'NONE',  ( -0.5073702590888615749, 0.9696319393318632018, -1.367288630523146420 ) ) ;
#67=CARTESIAN_POINT ( 'NONE',  ( 1.048552902599916292, 0.4330708661417427274, -1.573978973432617279 ) ) ;
#71=ORIENTED_EDGE ( 'NONE', *, *, #7518, .T. ) ;
#73=CARTESIAN_POINT ( 'NONE',  ( -0.4348450093584657061, -1.063161251382699124, -1.569784523562343992 ) ) ;
#75=VERTEX_POINT ( 'NONE', #2557 ) ;
#76=ORIENTED_EDGE ( 'NONE', *, *, #2854, .T. ) ;
#81=CARTESIAN_POINT ( 'NONE',  ( 0.4999746636856467474, 0.9773775067402665773, -1.373988502838978665 ) ) ;
#82=ORIENTED_EDGE ( 'NONE', *, *, #3467, .F. ) ;
#90=VECTOR ( 'NONE', #7074, 39.37007874015748143 ) ;
#98=AXIS2_PLACEMENT_3D ( 'NONE', #2181, #4591, #4516 ) ;
#100=CARTESIAN_POINT ( 'NONE',  ( -0.4437902010346558290, 0.9221077491748241872, -1.453484313640523107 ) ) ;
#102=DIRECTION ( 'NONE',  ( -1.000000000000000000, 0.000000000000000000, 0.000000000000000000 ) ) ;
#106=CARTESIAN_POINT ( 'NONE',  ( -0.4349192958999751890, 0.9810556462971158354, -1.448591228719268820 ) ) ;
#112=FACE_OUTER_BOUND ( 'NONE', #858, .T. ) ;
#114=ORIENTED_EDGE ( 'NONE', *, *, #6223, .T. ) ;
#116=CARTESIAN_POINT ( 'NONE',  ( -0.5141614760841455301, -1.056523642887403414, -1.484898342931014081 ) ) ;
#117=B_SPLINE_CURVE_WITH_KNOTS ( 'NONE', 3,
 ( #3701, #1901, #4841, #4348, #5547, #6644, #2544, #3159, #6569, #5505, #6716, #789, #6606, #304, #7249, #1393, #4232, #1353 ),
 .UNSPECIFIED., .F., .F.,
 ( 4, 2, 2, 2, 2, 2, 2, 2, 4 ),
 ( 0.000000000000000000, 0.0002327816859446662134, 0.0004655633718893324269, 0.0009311267437786553127, 0.001396690115667978144, 0.001862253487557301085, 0.002327816859446624025, 0.002793380231335946748, 0.003724506975114579184 ),
 .UNSPECIFIED. ) ;
#128=ORIENTED_EDGE ( 'NONE', *, *, #6591, .F. ) ;
#133=CARTESIAN_POINT ( 'NONE',  ( 1.078368654584408670, -0.4878048847236703955, -1.510181419419386772 ) ) ;
#135=VERTEX_POINT ( 'NONE', #1514 ) ;
#146=CIRCLE ( 'NONE', #633, 1.043121362164705745 ) ;
#147=CARTESIAN_POINT ( 'NONE',  ( -0.8785537298370117432, -0.4700904924197938373, -1.433776001880364470 ) ) ;
#149=CARTESIAN_POINT ( 'NONE',  ( 0.5141614760841460852, -0.9609181420092316461, -1.361499588670819216 ) ) ;
#156=ADVANCED_FACE ( 'NONE', ( #5228 ), #2856, .T. ) ;
#157=CARTESIAN_POINT ( 'NONE',  ( 1.041228047528458989, -0.4333661275891970699, -1.574803149606299302 ) ) ;
#160=EDGE_CURVE ( 'NONE', #5534, #5278, #5680, .T. ) ;
#165=ORIENTED_EDGE ( 'NONE', *, *, #6591, .T. ) ;
#168=CIRCLE ( 'NONE', #5420, 1.278433327952054555 ) ;
#172=ORIENTED_EDGE ( 'NONE', *, *, #5240, .T. ) ;
#174=ORIENTED_EDGE ( 'NONE', *, *, #5753, .F. ) ;
#179=CARTESIAN_POINT ( 'NONE',  ( 1.080458355692619721, -0.4837911690062307035, -1.514208178040841846 ) ) ;
#180=CARTESIAN_POINT ( 'NONE',  ( -0.4466264210910796950, -0.9159926810392101659, -1.451746030331785509 ) ) ;
#185=CARTESIAN_POINT ( 'NONE',  ( -0.9159926810392086116, -0.4466264210910828036, -1.451746030331785509 ) ) ;
#186=FACE_OUTER_BOUND ( 'NONE', #1523, .T. ) ;
#189=CARTESIAN_POINT ( 'NONE',  ( 1.084813347358858593, 0.4713815370807524219, -1.526966122205014820 ) ) ;
#195=ORIENTED_EDGE ( 'NONE', *, *, #3184, .F. ) ;
#196=CARTESIAN_POINT ( 'NONE',  ( -0.9609181420092336445, 0.5141614760841427545, -1.361499588670819216 ) ) ;
#200=ADVANCED_FACE ( 'NONE', ( #5743 ), #3325, .T. ) ;
#201=ADVANCED_FACE ( 'NONE', ( #6803 ), #1631, .T. ) ;
#215=B_SPLINE_CURVE_WITH_KNOTS ( 'NONE', 3,
 ( #4148, #5462, #5874, #221, #2542, #2507, #3617, #677, #5336, #2427, #1312, #7093, #1857, #4839, #714, #747, #3037, #5380 ),
 .UNSPECIFIED., .F., .F.,
 ( 4, 2, 2, 2, 2, 2, 2, 2, 4 ),
 ( 0.000000000000000000, 0.0002327816859446665387, 0.0004655633718893330774, 0.0009311267437786566138, 0.001396690115667980096, 0.001862253487557303687, 0.002327816859446627060, 0.002793380231335950651, 0.003724506975114584388 ),
 .UNSPECIFIED. ) ;
#221=CARTESIAN_POINT ( 'NONE',  ( -1.060348472569316414, 0.4341579012690653383, -1.570964862939435491 ) ) ;
#227=CARTESIAN_POINT ( 'NONE',  ( -0.9609181420092316461, -0.5141614760841496379, -1.361499588670821659 ) ) ;
#231=DIRECTION ( 'NONE',  ( -1.047444401652940007E-14, 1.000000000000000000, -0.000000000000000000 ) ) ;
#237=CIRCLE ( 'NONE', #7423, 1.223643328182682621 ) ;
#243=CIRCLE ( 'NONE', #5500, 1.089828288828796676 ) ;
#244=CARTESIAN_POINT ( 'NONE',  ( 0.4338950423154144254, -1.037563309807725043, -1.574803149606299302 ) ) ;
#246=EDGE_CURVE ( 'NONE', #5720, #477, #3388, .T. ) ;
#248=ORIENTED_EDGE ( 'NONE', *, *, #5809, .F. ) ;
#251=( NAMED_UNIT ( * ) PLANE_ANGLE_UNIT ( ) SI_UNIT ( $, .RADIAN. ) );
#252=CARTESIAN_POINT ( 'NONE',  ( 0.9666437042230172638, -0.4330708661417221883, -1.454455828411335583 ) ) ;
#267=CARTESIAN_POINT ( 'NONE',  ( -0.4544645342395071674, 0.9861598787149296053, -1.560495034967182670 ) ) ;
#269=VERTEX_POINT ( 'NONE', #2475 ) ;
#272=CARTESIAN_POINT ( 'NONE',  ( -0.4470331066954956190, 1.081428707249768362, -1.553789012478534959 ) ) ;
#277=CARTESIAN_POINT ( 'NONE',  ( -0.4330708661417317362, -1.044891351410288438, -1.574550377471545914 ) ) ;
#281=AXIS2_PLACEMENT_3D ( 'NONE', #6819, #5069, #5106 ) ;
#283=VERTEX_POINT ( 'NONE', #1196 ) ;
#287=EDGE_CURVE ( 'NONE', #5534, #7462, #1651, .T. ) ;
#289=ORIENTED_EDGE ( 'NONE', *, *, #5761, .F. ) ;
#291=ORIENTED_EDGE ( 'NONE', *, *, #6914, .T. ) ;
#298=EDGE_CURVE ( 'NONE', #1329, #4949, #6196, .T. ) ;
#304=CARTESIAN_POINT ( 'NONE',  ( 0.4837908950006664655, -1.080458485393811729, -1.514208454829284234 ) ) ;
#308=DIRECTION ( 'NONE',  ( -2.312579046053608732E-29, 2.207829878515936732E-15, 1.000000000000000000 ) ) ;
#309=CARTESIAN_POINT ( 'NONE',  ( -0.4509662133831515707, 0.9917530546321599028, -1.563429817131423372 ) ) ;
#313=DIRECTION ( 'NONE',  ( -0.000000000000000000, -0.000000000000000000, 1.000000000000000000 ) ) ;
#318=DIRECTION ( 'NONE',  ( 0.000000000000000000, -4.647695938698650194E-15, 1.000000000000000000 ) ) ;
#319=ORIENTED_EDGE ( 'NONE', *, *, #4766, .T. ) ;
#320=CARTESIAN_POINT ( 'NONE',  ( 0.4700904924197906176, -0.9659644734970541657, -1.546597720061111847 ) ) ;
#323=CARTESIAN_POINT ( 'NONE',  ( -0.4330708661417322913, 0.9666437042230143772, -1.454455828411337359 ) ) ;
#324=CARTESIAN_POINT ( 'NONE',  ( 0.4330708661417322913, -1.048552902599920289, -1.573978973432616835 ) ) ;
#325=CARTESIAN_POINT ( 'NONE',  ( 0.9984400756355499285, -0.4637694296357074975, -1.410742812766314414 ) ) ;
#330=ORIENTED_EDGE ( 'NONE', *, *, #1146, .F. ) ;
#337=DIRECTION ( 'NONE',  ( -1.000000000000000000, -8.881784197001252323E-16, 0.000000000000000000 ) ) ;
#341=CARTESIAN_POINT ( 'NONE',  ( 0.4330708661417322913, 1.048552902599920289, -1.573978973432616835 ) ) ;
#345=VERTEX_POINT ( 'NONE', #7020 ) ;
#346=MECHANICAL_DESIGN_GEOMETRIC_PRESENTATION_REPRESENTATION('',(#1785),#5726);
#347=CARTESIAN_POINT ( 'NONE',  ( -0.9971723906835432416, 0.4475999628372159256, -1.429777239771657049 ) ) ;
#355=CARTESIAN_POINT ( 'NONE',  ( 0.4617902729098475878, -0.9752011746066220343, -1.554226146211406423 ) ) ;
#356=AXIS2_PLACEMENT_3D ( 'NONE', #2044, #3186, #894 ) ;
#365=CARTESIAN_POINT ( 'NONE',  ( -1.795185198899834826E-15, 0.5141614760841457521, -2.204724409448820754 ) ) ;
#377=ADVANCED_FACE ( 'NONE', ( #186 ), #5685, .F. ) ;
#380=AXIS2_PLACEMENT_3D ( 'NONE', #4053, #3479, #6788 ) ;
#382=EDGE_CURVE ( 'NONE', #2732, #3031, #1272, .T. ) ;
#383=VERTEX_POINT ( 'NONE', #4689 ) ;
#390=CARTESIAN_POINT ( 'NONE',  ( -0.9895441027518975252, -0.4843356560173227576, -1.389133886014303654 ) ) ;
#391=ORIENTED_EDGE ( 'NONE', *, *, #2568, .F. ) ;
#403=CARTESIAN_POINT ( 'NONE',  ( 0.4338950423154144254, 1.037563309807724821, -1.574803149606299302 ) ) ;
#408=VERTEX_POINT ( 'NONE', #1981 ) ;
#409=CIRCLE ( 'NONE', #3943, 1.278433327952055887 ) ;
#415=AXIS2_PLACEMENT_3D ( 'NONE', #4819, #7026, #1709 ) ;
#416=DIRECTION ( 'NONE',  ( 0.000000000000000000, -4.615976749461841764E-15, 1.000000000000000000 ) ) ;
#418=CARTESIAN_POINT ( 'NONE',  ( 0.000000000000000000, 0.000000000000000000, 0.000000000000000000 ) ) ;
#419=CARTESIAN_POINT ( 'NONE',  ( 0.000000000000000000, 0.000000000000000000, -1.546597720061111847 ) ) ;
#422=CARTESIAN_POINT ( 'NONE',  ( 1.023372273685344114, -0.4368378848980421503, -1.573834172653142627 ) ) ;
#423=DIRECTION ( 'NONE',  ( 0.000000000000000000, 0.000000000000000000, 1.000000000000000000 ) ) ;
#425=CARTESIAN_POINT ( 'NONE',  ( -0.4338950423154138147, 1.037563309807725043, -1.574803149606299302 ) ) ;
#434=EDGE_LOOP ( 'NONE', ( #1915, #6428, #3869, #6323 ) ) ;
#438=APPLICATION_CONTEXT ( 'automotive_design' ) ;
#440=ADVANCED_FACE ( 'NONE', ( #4884 ), #5559, .T. ) ;
#441=ADVANCED_FACE ( 'NONE', ( #1579 ), #4944, .F. ) ;
#442=ORIENTED_EDGE ( 'NONE', *, *, #702, .F. ) ;
#443=VERTEX_POINT ( 'NONE', #5112 ) ;
#451=CARTESIAN_POINT ( 'NONE',  ( 0.000000000000000000, 0.000000000000000000, -0.7983802283864783744 ) ) ;
#457=B_SPLINE_CURVE_WITH_KNOTS ( 'NONE', 3,
 ( #7261, #6093, #2034, #3246, #847, #5522, #7295, #3212, #1442, #883, #1478, #3832, #6164, #4825, #7148, #4247, #6583, #1332 ),
 .UNSPECIFIED., .F., .F.,
 ( 4, 2, 2, 2, 2, 2, 2, 2, 4 ),
 ( -8.042425861382277794E-06, 0.0009212656149224035746, 0.001385919635314291623, 0.001850573655706179562, 0.002315227676098066852, 0.002779881696489955225, 0.003244535716881843165, 0.003476862727077782798, 0.003709189737273722864 ),
 .UNSPECIFIED. ) ;
#459=EDGE_CURVE ( 'NONE', #2045, #4474, #3812, .T. ) ;
#471=CARTESIAN_POINT ( 'NONE',  ( -0.9697097640641200167, -0.4330708661417358440, -1.453662949853145481 ) ) ;
#476=AXIS2_PLACEMENT_3D ( 'NONE', #6453, #2355, #607 ) ;
#477=VERTEX_POINT ( 'NONE', #6294 ) ;
#487=CARTESIAN_POINT ( 'NONE',  ( -0.8785537298370134085, 0.4700904924197875645, -1.433776001880362250 ) ) ;
#495=CARTESIAN_POINT ( 'NONE',  ( 0.000000000000000000, 0.000000000000000000, -0.8561751947315059397 ) ) ;
#510=CARTESIAN_POINT ( 'NONE',  ( -0.9666437042230129340, -0.4330708661417356220, -1.454455828411337359 ) ) ;
#514=ORIENTED_EDGE ( 'NONE', *, *, #5753, .T. ) ;
#515=CIRCLE ( 'NONE', #3926, 1.174991162294038993 ) ;
#519=ORIENTED_EDGE ( 'NONE', *, *, #1924, .T. ) ;
#525=ADVANCED_FACE ( 'NONE', ( #5728 ), #53, .T. ) ;
#530=AXIS2_PLACEMENT_3D ( 'NONE', #2041, #6853, #2680 ) ;
#546=ORIENTED_EDGE ( 'NONE', *, *, #1729, .T. ) ;
#547=ORIENTED_EDGE ( 'NONE', *, *, #3754, .F. ) ;
#551=CARTESIAN_POINT ( 'NONE',  ( 0.4700904924197903956, 0.000000000000000000, -2.204724409448820754 ) ) ;
#557=CARTESIAN_POINT ( 'NONE',  ( -0.9604263920613177463, -0.4330708661417355665, -1.456063616177416087 ) ) ;
#564=CARTESIAN_POINT ( 'NONE',  ( -5.154746071126634886E-15, 0.4921259842519648542, -2.204724409448822975 ) ) ;
#567=CARTESIAN_POINT ( 'NONE',  ( 0.4332839536939404601, -0.9726683636255515353, -1.452651081959918544 ) ) ;
#571=EDGE_CURVE ( 'NONE', #1688, #735, #1032, .T. ) ;
#573=CARTESIAN_POINT ( 'NONE',  ( -0.4375700189966297837, -1.070856827570679570, -1.565644132322242532 ) ) ;
#574=CARTESIAN_POINT ( 'NONE',  ( -1.718248690375557255E-15, 0.4921259842519683514, -2.204724409448820754 ) ) ;
#576=ORIENTED_EDGE ( 'NONE', *, *, #2847, .T. ) ;
#581=DIRECTION ( 'NONE',  ( 0.000000000000000000, 0.000000000000000000, -1.000000000000000000 ) ) ;
#583=AXIS2_PLACEMENT_3D ( 'NONE', #5101, #7419, #5821 ) ;
#584=CARTESIAN_POINT ( 'NONE',  ( -1.003668447264492558, 0.4445641707282946831, -1.568529612473645862 ) ) ;
#586=ORIENTED_EDGE ( 'NONE', *, *, #2666, .T. ) ;
#595=ORIENTED_EDGE ( 'NONE', *, *, #2941, .T. ) ;
#597=CARTESIAN_POINT ( 'NONE',  ( 0.4700904924197906176, -0.8785537298370117432, -1.433776001880362250 ) ) ;
#605=CARTESIAN_POINT ( 'NONE',  ( 0.4559220466128925953, -0.8989365377700702098, -1.445239289764781665 ) ) ;
#607=DIRECTION ( 'NONE',  ( 0.000000000000000000, -1.000000000000000000, 2.095133389269358970E-15 ) ) ;
#617=DIRECTION ( 'NONE',  ( 0.000000000000000000, 0.000000000000000000, -1.000000000000000000 ) ) ;
#619=ORIENTED_EDGE ( 'NONE', *, *, #7330, .F. ) ;
#630=VERTEX_POINT ( 'NONE', #5218 ) ;
#632=CARTESIAN_POINT ( 'NONE',  ( -0.9752011746066392428, -0.4617902729099834236, -1.554226146211527881 ) ) ;
#633=AXIS2_PLACEMENT_3D ( 'NONE', #1426, #6154, #2659 ) ;
#641=CARTESIAN_POINT ( 'NONE',  ( 0.5073440712904525585, -0.9696655408444868618, -1.367310953805774831 ) ) ;
#642=CARTESIAN_POINT ( 'NONE',  ( -0.4882980771758828609, 0.9867934559254231131, -1.385219299502222112 ) ) ;
#648=DIRECTION ( 'NONE',  ( -1.000000000000000000, -8.881784197001252323E-16, -2.256009703088257329E-15 ) ) ;
#650=CIRCLE ( 'NONE', #1623, 0.9964144355006140374 ) ;
#653=CARTESIAN_POINT ( 'NONE',  ( -0.5141614760841455301, -1.056523642887403414, -1.484898342931014081 ) ) ;
#654=ORIENTED_EDGE ( 'NONE', *, *, #3315, .F. ) ;
#666=CARTESIAN_POINT ( 'NONE',  ( -1.048552902599919401, -0.4330708661417353444, -1.573978973432617279 ) ) ;
#667=DIRECTION ( 'NONE',  ( -1.000000000000000000, -0.000000000000000000, -4.625929269271482167E-15 ) ) ;
#675=( NAMED_UNIT ( * ) PLANE_ANGLE_UNIT ( ) SI_UNIT ( $, .RADIAN. ) );
#677=CARTESIAN_POINT ( 'NONE',  ( -1.081428632361003839, 0.4470329974975731924, -1.553789141944099894 ) ) ;
#678=CARTESIAN_POINT ( 'NONE',  ( 5.154746071126671174E-15, -0.4921259842519683514, -2.204724409448820754 ) ) ;
#686=DIRECTION ( 'NONE',  ( -1.000000000000000000, 0.000000000000000000, 0.000000000000000000 ) ) ;
#688=EDGE_LOOP ( 'NONE', ( #319, #4284, #3558, #6790 ) ) ;
#690=CARTESIAN_POINT ( 'NONE',  ( 0.000000000000000000, 0.000000000000000000, -1.515748031496062964 ) ) ;
#700=CARTESIAN_POINT ( 'NONE',  ( 0.4339190921229452713, -0.9541934910893031807, -1.456692913385827071 ) ) ;
#702=EDGE_CURVE ( 'NONE', #3366, #1329, #5656, .T. ) ;
#709=VERTEX_POINT ( 'NONE', #5413 ) ;
#710=TOROIDAL_SURFACE ( 'NONE', #4988, 1.043121362164705745, 0.05905511811023622659 ) ;
#714=CARTESIAN_POINT ( 'NONE',  ( -1.078368813366572310, 0.4878045971889936605, -1.510181706589752482 ) ) ;
#718=CARTESIAN_POINT ( 'NONE',  ( 0.4663806185493042933, -0.8833138556570224731, -1.436938405272258246 ) ) ;
#727=DIRECTION ( 'NONE',  ( 0.000000000000000000, 1.000000000000000000, 2.256009703088257329E-15 ) ) ;
#730=AXIS2_PLACEMENT_3D ( 'NONE', #3349, #2774, #2203 ) ;
#735=VERTEX_POINT ( 'NONE', #2004 ) ;
#742=CARTESIAN_POINT ( 'NONE',  ( -1.048552902599919401, -0.4330708661417353444, -1.573978973432617279 ) ) ;
#743=DIRECTION ( 'NONE',  ( 0.000000000000000000, 0.000000000000000000, -1.000000000000000000 ) ) ;
#747=CARTESIAN_POINT ( 'NONE',  ( -1.070877820178679052, 0.4996352642496060814, -1.498503547059352181 ) ) ;
#755=DIRECTION ( 'NONE',  ( 0.000000000000000000, 0.000000000000000000, 1.000000000000000000 ) ) ;
#761=DIRECTION ( 'NONE',  ( -1.000000000000000000, 0.000000000000000000, 0.000000000000000000 ) ) ;
#762=CARTESIAN_POINT ( 'NONE',  ( 1.718248690375545225E-15, -0.4921259842519648542, -2.204724409448822975 ) ) ;
#767=ORIENTED_EDGE ( 'NONE', *, *, #2252, .F. ) ;
#774=ORIENTED_EDGE ( 'NONE', *, *, #4146, .T. ) ;
#781=VERTEX_POINT ( 'NONE', #3604 ) ;
#788=CARTESIAN_POINT ( 'NONE',  ( -0.4388996395293570107, 0.9346850374427959629, -1.455943645409048637 ) ) ;
#789=CARTESIAN_POINT ( 'NONE',  ( 0.4713813068963902952, -1.084813395429188088, -1.526966363676887317 ) ) ;
#807=ADVANCED_FACE ( 'NONE', ( #6519 ), #1567, .F. ) ;
#811=VERTEX_POINT ( 'NONE', #3253 ) ;
#818=CARTESIAN_POINT ( 'NONE',  ( 0.9609181420092369752, -0.5141614760841358711, -1.361499588670819216 ) ) ;
#822=DIRECTION ( 'NONE',  ( -2.312579046053608732E-29, 2.207829878515936732E-15, 1.000000000000000000 ) ) ;
#827=AXIS2_PLACEMENT_3D ( 'NONE', #4003, #1086, #6905 ) ;
#833=CARTESIAN_POINT ( 'NONE',  ( 0.8884022185686345496, -0.4627504720074674949, -1.439912370850673806 ) ) ;
#837=CARTESIAN_POINT ( 'NONE',  ( 1.023371766162640473, 0.4368380215374228492, -1.573834103987475475 ) ) ;
#841=CARTESIAN_POINT ( 'NONE',  ( -0.4996355910473242457, 1.070877566692229221, -1.498503231159225457 ) ) ;
#847=CARTESIAN_POINT ( 'NONE',  ( 0.4837911690062421388, 1.080458355692614614, -1.514208178040841180 ) ) ;
#848=ORIENTED_EDGE ( 'NONE', *, *, #702, .T. ) ;
#849=TOROIDAL_SURFACE ( 'NONE', #4129, 1.223643328182682621, 0.05905511811023622659 ) ;
#858=EDGE_LOOP ( 'NONE', ( #6817, #174, #897, #1527, #4829, #1104 ) ) ;
#862=FACE_OUTER_BOUND ( 'NONE', #1840, .T. ) ;
#863=ORIENTED_EDGE ( 'NONE', *, *, #382, .F. ) ;
#875=CARTESIAN_POINT ( 'NONE',  ( -0.9984401429152555130, 0.4637690556582312329, -1.410743228759549828 ) ) ;
#876=CARTESIAN_POINT ( 'NONE',  ( -0.4713815370807409866, 1.084813347358863700, -1.526966122205014820 ) ) ;
#883=CARTESIAN_POINT ( 'NONE',  ( 0.4508657589754702655, 1.083410700381145508, -1.549345605342071774 ) ) ;
#886=DIRECTION ( 'NONE',  ( 1.000000000000000000, 1.049299683535328711E-14, 0.000000000000000000 ) ) ;
#888=ORIENTED_EDGE ( 'NONE', *, *, #7418, .T. ) ;
#893=ADVANCED_FACE ( 'NONE', ( #1524 ), #6865, .T. ) ;
#894=DIRECTION ( 'NONE',  ( -1.000000000000000000, -1.047444401652940007E-14, -6.779428194327236205E-32 ) ) ;
#895=ORIENTED_EDGE ( 'NONE', *, *, #1257, .T. ) ;
#897=ORIENTED_EDGE ( 'NONE', *, *, #2246, .F. ) ;
#908=CARTESIAN_POINT ( 'NONE',  ( 0.000000000000000000, 0.000000000000000000, -1.574803149606299302 ) ) ;
#910=CARTESIAN_POINT ( 'NONE',  ( 0.4663632139996677362, 0.8833361873720626534, -1.436953241411902837 ) ) ;
#911=CARTESIAN_POINT ( 'NONE',  ( 0.000000000000000000, 0.000000000000000000, -3.582716535433073002 ) ) ;
#914=CARTESIAN_POINT ( 'NONE',  ( -1.861696953619914682E-15, 0.000000000000000000, -1.361499588670820771 ) ) ;
#928=CARTESIAN_POINT ( 'NONE',  ( -0.4330708661417287941, 0.000000000000000000, -2.204724409448822975 ) ) ;
#938=B_SPLINE_CURVE_WITH_KNOTS ( 'NONE', 3,
 ( #3301, #6822, #700, #7081 ),
 .UNSPECIFIED., .F., .F.,
 ( 4, 4 ),
 ( 0.000000000000000000, 0.0004815725036528474990 ),
 .UNSPECIFIED. ) ;
#945=CARTESIAN_POINT ( 'NONE',  ( 0.000000000000000000, 0.000000000000000000, -2.204724409448820754 ) ) ;
#950=CARTESIAN_POINT ( 'NONE',  ( 0.9755734897585840448, 0.4619485889667721001, -1.553989674004691901 ) ) ;
#953=CIRCLE ( 'NONE', #4610, 1.174991162294038771 ) ;
#955=ORIENTED_EDGE ( 'NONE', *, *, #1246, .T. ) ;
#966=DIRECTION ( 'NONE',  ( -1.000000000000000000, -3.491481338843133355E-15, 0.000000000000000000 ) ) ;
#971=ORIENTED_EDGE ( 'NONE', *, *, #2285, .T. ) ;
#981=CARTESIAN_POINT ( 'NONE',  ( 0.4353079511162236126, 0.9479499796399308842, -1.456692913385826849 ) ) ;
#982=DIRECTION ( 'NONE',  ( 0.000000000000000000, 0.000000000000000000, 1.000000000000000000 ) ) ;
#984=DIRECTION ( 'NONE',  ( -1.000000000000000000, -0.000000000000000000, -4.625929269271482167E-15 ) ) ;
#985=CARTESIAN_POINT ( 'NONE',  ( 0.9917530546321550178, 0.4509662133831619513, -1.563429817131423372 ) ) ;
#986=EDGE_CURVE ( 'NONE', #4949, #1484, #5409, .T. ) ;
#987=ORIENTED_EDGE ( 'NONE', *, *, #3793, .T. ) ;
#991=CARTESIAN_POINT ( 'NONE',  ( -0.9411660957780404457, 0.4368170150760360415, -1.456692913385826849 ) ) ;
#993=CIRCLE ( 'NONE', #1973, 0.2362204724409449341 ) ;
#996=CARTESIAN_POINT ( 'NONE',  ( -0.9479499796399307732, -0.4353079511162269433, -1.456692913385828625 ) ) ;
#1003=CARTESIAN_POINT ( 'NONE',  ( 0.9921524035015003573, 0.4406690496059847972, -1.439080679658374384 ) ) ;
#1007=ORIENTED_EDGE ( 'NONE', *, *, #4073, .F. ) ;
#1010=ORIENTED_EDGE ( 'NONE', *, *, #5672, .F. ) ;
#1016=TOROIDAL_SURFACE ( 'NONE', #5285, 1.043121362164705745, 0.05905511811023622659 ) ;
#1019=CARTESIAN_POINT ( 'NONE',  ( 0.9159926810392130525, -0.4466264210910701471, -1.451746030331783510 ) ) ;
#1025=AXIS2_PLACEMENT_3D ( 'NONE', #5708, #3980, #2817 ) ;
#1026=ORIENTED_EDGE ( 'NONE', *, *, #5761, .T. ) ;
#1031=B_SPLINE_CURVE_WITH_KNOTS ( 'NONE', 3,
 ( #2435, #718, #5924, #605, #6410, #4115, #3621, #7100, #5266, #3543 ),
 .UNSPECIFIED., .F., .F.,
 ( 4, 2, 2, 2, 4 ),
 ( -7.765797721852544519E-06, 0.0005114169989440498724, 0.001030599795609952150, 0.001549782592275854428, 0.002068965388941757140 ),
 .UNSPECIFIED. ) ;
#1032=CIRCLE ( 'NONE', #7255, 0.9964144355006141485 ) ;
#1046=DIRECTION ( 'NONE',  ( 4.647695938698652561E-15, 0.000000000000000000, -1.000000000000000000 ) ) ;
#1050=CARTESIAN_POINT ( 'NONE',  ( 0.8833361873720787516, 0.4663632139997673232, -1.436953241411981663 ) ) ;
#1052=DIRECTION ( 'NONE',  ( -1.224646799147353207E-16, -1.000000000000000000, -0.000000000000000000 ) ) ;
#1054=CARTESIAN_POINT ( 'NONE',  ( -0.5072022184711438841, -1.064268091467010846, -1.491294347567248435 ) ) ;
#1072=ORIENTED_EDGE ( 'NONE', *, *, #4997, .T. ) ;
#1073=CARTESIAN_POINT ( 'NONE',  ( -1.861696953619914682E-15, 0.000000000000000000, -1.361499588670820771 ) ) ;
#1075=CIRCLE ( 'NONE', #7179, 1.089828288828796676 ) ;
#1079=VERTEX_POINT ( 'NONE', #3135 ) ;
#1080=ORIENTED_EDGE ( 'NONE', *, *, #6315, .F. ) ;
#1086=DIRECTION ( 'NONE',  ( 1.000000000000000000, 0.000000000000000000, -0.000000000000000000 ) ) ;
#1091=CARTESIAN_POINT ( 'NONE',  ( -1.781909941321919274E-15, 0.000000000000000000, -1.397637795275591843 ) ) ;
#1093=CARTESIAN_POINT ( 'NONE',  ( 0.000000000000000000, 0.000000000000000000, -0.7983802283864780414 ) ) ;
#1094=DIRECTION ( 'NONE',  ( 1.000000000000000000, 0.000000000000000000, -0.000000000000000000 ) ) ;
#1104=ORIENTED_EDGE ( 'NONE', *, *, #7014, .F. ) ;
#1116=AXIS2_PLACEMENT_3D ( 'NONE', #678, #3002, #5337 ) ;
#1120=AXIS2_PLACEMENT_3D ( 'NONE', #5408, #3520, #581 ) ;
#1131=ORIENTED_EDGE ( 'NONE', *, *, #5382, .T. ) ;
#1146=EDGE_CURVE ( 'NONE', #735, #5146, #6301, .T. ) ;
#1156=CARTESIAN_POINT ( 'NONE',  ( -0.4700904924197903401, -0.9659644734970543878, -1.546597720061111847 ) ) ;
#1157=CARTESIAN_POINT ( 'NONE',  ( -0.4377665650305635481, 0.9883301303667336724, -1.443420399700355850 ) ) ;
#1167=CIRCLE ( 'NONE', #4113, 1.278433327952056553 ) ;
#1171=AXIS2_PLACEMENT_3D ( 'NONE', #3053, #2405, #4741 ) ;
#1180=CARTESIAN_POINT ( 'NONE',  ( -0.4437903857718329403, -0.9221073153504530939, -1.453484209829405849 ) ) ;
#1181=ORIENTED_EDGE ( 'NONE', *, *, #5950, .T. ) ;
#1186=B_SPLINE_CURVE_WITH_KNOTS ( 'NONE', 3,
 ( #818, #2645, #3258, #7268, #4908, #6740, #4372, #325, #1491, #3842, #3764, #1382, #6066, #6173, #6706, #1451, #6672, #252 ),
 .UNSPECIFIED., .F., .F.,
 ( 4, 2, 2, 2, 2, 2, 2, 2, 4 ),
 ( -8.121667112575779769E-06, 0.0009422843086939633418, 0.001417487296597240952, 0.001892690284500518237, 0.002367893272403795522, 0.002843096260307073023, 0.003318299248210350091, 0.003555900742161984072, 0.003793502236113618052 ),
 .UNSPECIFIED. ) ;
#1187=SHAPE_REPRESENTATION_RELATIONSHIP ( 'NONE' , 'NONE' ,  #2104, #2576 ) ;
#1192=TOROIDAL_SURFACE ( 'NONE', #2547, 1.124634398195722973, 0.05905511811023622659 ) ;
#1193=DIRECTION ( 'NONE',  ( -1.000000000000000000, -1.776356839400250465E-15, 0.000000000000000000 ) ) ;
#1196=CARTESIAN_POINT ( 'NONE',  ( -0.4353079511162236681, -0.9479499796399322165, -1.456692913385828625 ) ) ;
#1200=EDGE_CURVE ( 'NONE', #709, #5935, #5666, .T. ) ;
#1203=ORIENTED_EDGE ( 'NONE', *, *, #3271, .T. ) ;
#1206=DIRECTION ( 'NONE',  ( -0.000000000000000000, -0.000000000000000000, 1.000000000000000000 ) ) ;
#1211=EDGE_LOOP ( 'NONE', ( #3226, #6021, #4866, #3846 ) ) ;
#1213=TOROIDAL_SURFACE ( 'NONE', #4042, 1.223643328182682621, 0.05905511811023622659 ) ;
#1222=CARTESIAN_POINT ( 'NONE',  ( -1.054581703806070525, -0.4332776154273933478, -1.572814851683855597 ) ) ;
#1225=DIRECTION ( 'NONE',  ( -1.000000000000000000, 0.000000000000000000, -2.193342766891360832E-15 ) ) ;
#1226=CARTESIAN_POINT ( 'NONE',  ( -0.4333661275892026765, 1.041228047528455658, -1.574803149606299302 ) ) ;
#1227=ORIENTED_EDGE ( 'NONE', *, *, #7241, .T. ) ;
#1229=CARTESIAN_POINT ( 'NONE',  ( 0.9479499796399352141, -0.4353079511162137316, -1.456692913385826849 ) ) ;
#1230=DIRECTION ( 'NONE',  ( -1.000000000000000000, 0.000000000000000000, 0.000000000000000000 ) ) ;
#1235=CARTESIAN_POINT ( 'NONE',  ( -0.9541934910893046240, 0.4339190921229418296, -1.456692913385826849 ) ) ;
#1237=CARTESIAN_POINT ( 'NONE',  ( -0.4700904924197871204, 0.000000000000000000, -2.204724409448822975 ) ) ;
#1240=DIRECTION ( 'NONE',  ( -0.000000000000000000, -0.000000000000000000, 1.000000000000000000 ) ) ;
#1246=EDGE_CURVE ( 'NONE', #3477, #1972, #5940, .T. ) ;
#1257=EDGE_CURVE ( 'NONE', #2327, #5278, #5181, .T. ) ;
#1272=B_SPLINE_CURVE_WITH_KNOTS ( 'NONE', 3,
 ( #1156, #1862, #2352, #1317, #6534, #3620, #5962, #3042 ),
 .UNSPECIFIED., .F., .F.,
 ( 4, 2, 2, 4 ),
 ( -7.690028535482676563E-06, 0.001102852776893268553, 0.001658124179607648385, 0.002213395582322028217 ),
 .UNSPECIFIED. ) ;
#1274=PRODUCT_DEFINITION_CONTEXT ( 'detailed design', #438, 'design' ) ;
#1275=CARTESIAN_POINT ( 'NONE',  ( 0.4882975260543730434, -0.9867938558989103326, -1.385219839936550956 ) ) ;
#1304=B_SPLINE_CURVE_WITH_KNOTS ( 'NONE', 3,
 ( #742, #54, #1222, #4140, #7086, #4754, #7161, #2377, #3608, #6434, #3570, #6477, #1846, #4678, #4798, #5912, #3069, #6562 ),
 .UNSPECIFIED., .F., .F.,
 ( 4, 2, 2, 2, 2, 2, 2, 2, 4 ),
 ( 3.469446951953614189E-18, 0.0002327816859446636656, 0.0004655633718893238617, 0.0009311267437786459886, 0.001396690115667967953, 0.001862253487557290026, 0.002327816859446611882, 0.002793380231335934171, 0.003724506975114588291 ),
 .UNSPECIFIED. ) ;
#1306=ORIENTED_EDGE ( 'NONE', *, *, #5383, .F. ) ;
#1312=CARTESIAN_POINT ( 'NONE',  ( -1.085749034322391227, 0.4630669964643871483, -1.535808346805855429 ) ) ;
#1313=AXIS2_PLACEMENT_3D ( 'NONE', #762, #4930, #5931 ) ;
#1316=TOROIDAL_SURFACE ( 'NONE', #827, 1.223643328182681289, 0.05905511811023622659 ) ;
#1317=CARTESIAN_POINT ( 'NONE',  ( -0.4445636273010806772, -1.003669596044584722, -1.568530023225017223 ) ) ;
#1329=VERTEX_POINT ( 'NONE', #5509 ) ;
#1332=CARTESIAN_POINT ( 'NONE',  ( 0.4330708661417322913, 1.048552902599920289, -1.573978973432616835 ) ) ;
#1334=CARTESIAN_POINT ( 'NONE',  ( 0.4476001829033102175, 0.9971724964169970118, -1.429776958199368675 ) ) ;
#1337=ORIENTED_EDGE ( 'NONE', *, *, #459, .F. ) ;
#1340=CARTESIAN_POINT ( 'NONE',  ( -0.4339190921229451603, -0.9541934910893047350, -1.456692913385828625 ) ) ;
#1353=CARTESIAN_POINT ( 'NONE',  ( 0.5141614760841459741, -1.056523642887403192, -1.484898342931014303 ) ) ;
#1362=CARTESIAN_POINT ( 'NONE',  ( -1.651526287078852914E-15, 0.000000000000000000, -1.456692913385827515 ) ) ;
#1367=CARTESIAN_POINT ( 'NONE',  ( -0.5141614760841456411, 1.056523642887403414, -1.484898342931014303 ) ) ;
#1368=AXIS2_PLACEMENT_3D ( 'NONE', #1690, #1654, #4602 ) ;
#1379=ORIENTED_EDGE ( 'NONE', *, *, #1767, .T. ) ;
#1382=CARTESIAN_POINT ( 'NONE',  ( 0.9921524035015079068, -0.4406690496059638140, -1.439080679658372608 ) ) ;
#1389=AXIS2_PLACEMENT_3D ( 'NONE', #7168, #6647, #4270 ) ;
#1393=CARTESIAN_POINT ( 'NONE',  ( 0.4996352642496096341, -1.070877820178676831, -1.498503547059352403 ) ) ;
#1395=DIRECTION ( 'NONE',  ( 1.000000000000000000, 0.000000000000000000, 2.095133389269358970E-15 ) ) ;
#1402=CARTESIAN_POINT ( 'NONE',  ( -0.4330708661417316807, 1.051607560569806088, -1.573502278225820561 ) ) ;
#1405=FACE_OUTER_BOUND ( 'NONE', #7413, .T. ) ;
#1409=VERTEX_POINT ( 'NONE', #597 ) ;
#1426=CARTESIAN_POINT ( 'NONE',  ( 5.766273211944702482E-30, -1.651526287078852914E-15, -1.456692913385827515 ) ) ;
#1427=B_SPLINE_CURVE_WITH_KNOTS ( 'NONE', 3,
 ( #510, #471, #1518, #2673, #2716, #5173, #6888, #3864, #3906, #4477, #5091, #5677, #7484, #390, #2258, #6238, #4554, #3330 ),
 .UNSPECIFIED., .F., .F.,
 ( 4, 2, 2, 2, 2, 2, 2, 2, 4 ),
 ( 0.000000000000000000, 0.0002385177155853649095, 0.0004770354311707298190, 0.0009540708623414807799, 0.001431106293512231795, 0.001908141724682982810, 0.002385177155853733608, 0.002862212587024484840, 0.003816283449365995978 ),
 .UNSPECIFIED. ) ;
#1431=CARTESIAN_POINT ( 'NONE',  ( 0.9861598787149247203, 0.4544645342395175480, -1.560495034967182670 ) ) ;
#1433=CARTESIAN_POINT ( 'NONE',  ( -0.9697097640641210159, 0.4330708661417288496, -1.453662949853142594 ) ) ;
#1442=CARTESIAN_POINT ( 'NONE',  ( 0.4589126309195376008, 1.085572762089311416, -1.540322683979783669 ) ) ;
#1445=CARTESIAN_POINT ( 'NONE',  ( 4.536176542591472873E-15, -0.4330708661417322913, -2.204724409448820754 ) ) ;
#1449=AXIS2_PLACEMENT_3D ( 'NONE', #6996, #617, #3452 ) ;
#1451=CARTESIAN_POINT ( 'NONE',  ( 0.9726684123052360409, -0.4332839571663233968, -1.452651065350215154 ) ) ;
#1460=CARTESIAN_POINT ( 'NONE',  ( -0.9479499796399307732, -0.4353079511162269433, -1.456692913385828625 ) ) ;
#1463=CARTESIAN_POINT ( 'NONE',  ( 5.942930443104038687E-30, -1.702122929023921893E-15, -1.433776001880363582 ) ) ;
#1464=AXIS2_PLACEMENT_3D ( 'NONE', #2510, #3665, #1395 ) ;
#1467=DIRECTION ( 'NONE',  ( 1.047444401652940007E-14, -1.000000000000000000, 0.000000000000000000 ) ) ;
#1468=ORIENTED_EDGE ( 'NONE', *, *, #5382, .F. ) ;
#1470=CARTESIAN_POINT ( 'NONE',  ( -0.9960023578760586194, 0.4720886891211098502, -1.401719942879699143 ) ) ;
#1478=CARTESIAN_POINT ( 'NONE',  ( 0.4470331066954957855, 1.081428707249768140, -1.553789012478534959 ) ) ;
#1480=TOROIDAL_SURFACE ( 'NONE', #2470, 1.043121362164705745, 0.05905511811023622659 ) ;
#1484=VERTEX_POINT ( 'NONE', #6265 ) ;
#1485=EDGE_LOOP ( 'NONE', ( #4566, #4218, #6459, #3058, #1131, #2751 ) ) ;
#1487=CIRCLE ( 'NONE', #5898, 1.168853328413309134 ) ;
#1491=CARTESIAN_POINT ( 'NONE',  ( 0.9990286721055837704, -0.4596436929058785315, -1.415369458146013004 ) ) ;
#1492=VERTEX_POINT ( 'NONE', #5959 ) ;
#1507=LENGTH_MEASURE_WITH_UNIT ( LENGTH_MEASURE( 0.02539999999999999897 ), #7504 );
#1510=CARTESIAN_POINT ( 'NONE',  ( -0.4368380215374121356, 1.023371766162644914, -1.573834103987475475 ) ) ;
#1514=CARTESIAN_POINT ( 'NONE',  ( -0.4330708661417317362, -1.048552902599920955, -1.573978973432617279 ) ) ;
#1518=CARTESIAN_POINT ( 'NONE',  ( -0.9726683636255518683, -0.4332839536939438463, -1.452651081959920987 ) ) ;
#1520=CARTESIAN_POINT ( 'NONE',  ( 1.060348520640345571, -0.4341579107161988582, -1.570964845243104424 ) ) ;
#1521=FACE_OUTER_BOUND ( 'NONE', #5793, .T. ) ;
#1523=EDGE_LOOP ( 'NONE', ( #5727, #547, #165, #442 ) ) ;
#1524=FACE_OUTER_BOUND ( 'NONE', #2237, .T. ) ;
#1527=ORIENTED_EDGE ( 'NONE', *, *, #7279, .F. ) ;
#1533=ORIENTED_EDGE ( 'NONE', *, *, #6781, .F. ) ;
#1536=EDGE_CURVE ( 'NONE', #1079, #5576, #215, .T. ) ;
#1546=CARTESIAN_POINT ( 'NONE',  ( 0.4416276115803088875, 1.010073413237866147, -1.570717210673254538 ) ) ;
#1566=EDGE_LOOP ( 'NONE', ( #2501, #4241, #1650, #7410, #2975, #4490, #6140 ) ) ;
#1567=SPHERICAL_SURFACE ( 'NONE', #530, 1.259842519685039131 ) ;
#1568=CARTESIAN_POINT ( 'NONE',  ( 0.9773775067402629135, 0.4999746636856571835, -1.373988502838980885 ) ) ;
#1569=CIRCLE ( 'NONE', #5359, 1.174991162294038771 ) ;
#1578=CIRCLE ( 'NONE', #3909, 1.223643328182683065 ) ;
#1579=FACE_OUTER_BOUND ( 'NONE', #5139, .T. ) ;
#1582=CARTESIAN_POINT ( 'NONE',  ( 0.9411660957780360048, 0.4368170150760492532, -1.456692913385828847 ) ) ;
#1583=CARTESIAN_POINT ( 'NONE',  ( -0.9479499796399307732, -0.4353079511162269433, -1.456692913385828625 ) ) ;
#1584=AXIS2_PLACEMENT_3D ( 'NONE', #5075, #6531, #3616 ) ;
#1585=ADVANCED_FACE ( 'NONE', ( #1732 ), #1316, .T. ) ;
#1589=EDGE_CURVE ( 'NONE', #4488, #4463, #7305, .T. ) ;
#1595=DIRECTION ( 'NONE',  ( -2.207829878515936732E-15, 0.000000000000000000, 1.000000000000000000 ) ) ;
#1598=CARTESIAN_POINT ( 'NONE',  ( -0.8884031170519980369, 0.4627498550472156080, -1.439912866901231547 ) ) ;
#1599=CARTESIAN_POINT ( 'NONE',  ( 0.9604263920613221872, -0.4330708661417219663, -1.456063616177414310 ) ) ;
#1600=CIRCLE ( 'NONE', #2703, 1.168853328413308690 ) ;
#1602=CARTESIAN_POINT ( 'NONE',  ( -0.4921259842519648542, 0.000000000000000000, -2.204724409448822975 ) ) ;
#1616=DIRECTION ( 'NONE',  ( 0.000000000000000000, 0.000000000000000000, 1.000000000000000000 ) ) ;
#1617=EDGE_LOOP ( 'NONE', ( #5149, #4373, #767, #6843, #2822, #4828 ) ) ;
#1623=AXIS2_PLACEMENT_3D ( 'NONE', #6268, #1669, #2253 ) ;
#1626=EDGE_CURVE ( 'NONE', #283, #7001, #6146, .T. ) ;
#1631=TOROIDAL_SURFACE ( 'NONE', #6768, 1.124634398195722973, 0.05905511811023622659 ) ;
#1633=CARTESIAN_POINT ( 'NONE',  ( 0.4637690556582351187, -0.9984401429152542917, -1.410743228759550050 ) ) ;
#1638=B_SPLINE_CURVE_WITH_KNOTS ( 'NONE', 3,
 ( #320, #355, #5524, #4859, #2037, #4364, #2603, #244 ),
 .UNSPECIFIED., .F., .F.,
 ( 4, 2, 2, 4 ),
 ( -7.690028535483255933E-06, 0.001102852776893270938, 0.001658124179607644699, 0.002213395582322018676 ),
 .UNSPECIFIED. ) ;
#1640=AXIS2_PLACEMENT_3D ( 'NONE', #2692, #5654, #2509 ) ;
#1644=CARTESIAN_POINT ( 'NONE',  ( -0.5141614760841456411, 1.056523642887403414, -1.484898342931014303 ) ) ;
#1650=ORIENTED_EDGE ( 'NONE', *, *, #2285, .F. ) ;
#1651=B_SPLINE_CURVE_WITH_KNOTS ( 'NONE', 3,
 ( #6002, #1235, #5840, #6571 ),
 .UNSPECIFIED., .F., .F.,
 ( 4, 4 ),
 ( 0.000000000000000000, 0.0004815725036528541126 ),
 .UNSPECIFIED. ) ;
#1653=ORIENTED_EDGE ( 'NONE', *, *, #986, .F. ) ;
#1654=DIRECTION ( 'NONE',  ( 0.000000000000000000, 0.000000000000000000, -1.000000000000000000 ) ) ;
#1656=ORIENTED_EDGE ( 'NONE', *, *, #4450, .T. ) ;
#1660=CARTESIAN_POINT ( 'NONE',  ( -0.9541934910893034028, -0.4339190921229485465, -1.456692913385828847 ) ) ;
#1667=DIRECTION ( 'NONE',  ( -1.000000000000000000, -1.047444401652940007E-14, -6.779428194327236205E-32 ) ) ;
#1669=DIRECTION ( 'NONE',  ( 2.207829878515936732E-15, -0.000000000000000000, -1.000000000000000000 ) ) ;
#1672=CARTESIAN_POINT ( 'NONE',  ( 0.4377664870282949594, -0.9883299873891294718, -1.443420526770071044 ) ) ;
#1688=VERTEX_POINT ( 'NONE', #7041 ) ;
#1690=CARTESIAN_POINT ( 'NONE',  ( 0.000000000000000000, 0.000000000000000000, -1.515748031496062964 ) ) ;
#1691=VERTEX_POINT ( 'NONE', #2990 ) ;
#1699=CIRCLE ( 'NONE', #1449, 1.074277634097406953 ) ;
#1705=CARTESIAN_POINT ( 'NONE',  ( 7.714310545810097206E-17, 0.000000000000000000, -0.9448818897637817349 ) ) ;
#1706=CARTESIAN_POINT ( 'NONE',  ( -0.4843356560173193159, -0.9895441027518994126, -1.389133886014304320 ) ) ;
#1709=DIRECTION ( 'NONE',  ( -1.000000000000000000, 0.000000000000000000, 0.000000000000000000 ) ) ;
#1713=CARTESIAN_POINT ( 'NONE',  ( 0.000000000000000000, 0.000000000000000000, 0.000000000000000000 ) ) ;
#1716=ADVANCED_FACE ( 'NONE', ( #2458 ), #5735, .T. ) ;
#1720=B_SPLINE_CURVE_WITH_KNOTS ( 'NONE', 3,
 ( #6704, #2682, #2043, #4337 ),
 .UNSPECIFIED., .F., .F.,
 ( 4, 4 ),
 ( 0.000000000000000000, 0.0002807012396509386419 ),
 .UNSPECIFIED. ) ;
#1723=ADVANCED_FACE ( 'NONE', ( #5951 ), #5843, .T. ) ;
#1729=EDGE_CURVE ( 'NONE', #135, #7001, #237, .T. ) ;
#1732=FACE_OUTER_BOUND ( 'NONE', #6506, .T. ) ;
#1740=DIRECTION ( 'NONE',  ( 1.000000000000000000, 3.505805126173554996E-15, 0.000000000000000000 ) ) ;
#1744=DIRECTION ( 'NONE',  ( 0.000000000000000000, 1.000000000000000000, -2.193342766891360832E-15 ) ) ;
#1747=AXIS2_PLACEMENT_3D ( 'NONE', #2218, #5089, #6950 ) ;
#1751=CARTESIAN_POINT ( 'NONE',  ( 0.4377665650305637701, 0.9883301303667320070, -1.443420399700354739 ) ) ;
#1753=ORIENTED_EDGE ( 'NONE', *, *, #7332, .T. ) ;
#1760=CARTESIAN_POINT ( 'NONE',  ( 1.085749034841586580, -0.4630671888207288367, -1.535808138920397026 ) ) ;
#1761=CARTESIAN_POINT ( 'NONE',  ( -0.4368170415251730332, -0.9411659768779440105, -1.456692913385828847 ) ) ;
#1767=EDGE_CURVE ( 'NONE', #3765, #383, #1186, .T. ) ;
#1774=CARTESIAN_POINT ( 'NONE',  ( -0.4406690496059741946, 0.9921524035015047982, -1.439080679658375050 ) ) ;
#1775=CARTESIAN_POINT ( 'NONE',  ( -1.641312181851277713E-15, 0.4700904924197903956, -2.204724409448820754 ) ) ;
#1785=STYLED_ITEM('',(#7566),#4033);
#1788=CARTESIAN_POINT ( 'NONE',  ( 0.4332839571663337774, 0.9726684123052319331, -1.452651065350215154 ) ) ;
#1792=VERTEX_POINT ( 'NONE', #5607 ) ;
#1803=CIRCLE ( 'NONE', #6100, 1.223643328182682621 ) ;
#1806=CARTESIAN_POINT ( 'NONE',  ( -0.4466261709646376366, 0.9159932075028757170, -1.451746187131335519 ) ) ;
#1824=CARTESIAN_POINT ( 'NONE',  ( 0.4700904924197906176, 0.8785537298370117432, -1.433776001880362250 ) ) ;
#1835=CARTESIAN_POINT ( 'NONE',  ( 0.4330708661417322913, 0.000000000000000000, -2.204724409448820754 ) ) ;
#1836=AXIS2_PLACEMENT_3D ( 'NONE', #7027, #1206, #3630 ) ;
#1840=EDGE_LOOP ( 'NONE', ( #595, #4326, #6030, #6207, #3019, #7426 ) ) ;
#1846=CARTESIAN_POINT ( 'NONE',  ( -1.083679103503826902, -0.4755998196564530378, -1.522578840002906997 ) ) ;
#1852=ORIENTED_EDGE ( 'NONE', *, *, #6180, .T. ) ;
#1857=CARTESIAN_POINT ( 'NONE',  ( -1.083679103503829788, 0.4755998196564457658, -1.522578840002907219 ) ) ;
#1862=CARTESIAN_POINT ( 'NONE',  ( -0.4617902729102595916, -0.9752011746066798770, -1.554226146211785009 ) ) ;
#1866=CARTESIAN_POINT ( 'NONE',  ( 1.063161309294315515, 0.4348450248026808906, -1.569784497862149797 ) ) ;
#1869=CARTESIAN_POINT ( 'NONE',  ( 0.000000000000000000, 0.000000000000000000, -1.515748031496062964 ) ) ;
#1871=VERTEX_POINT ( 'NONE', #403 ) ;
#1873=CARTESIAN_POINT ( 'NONE',  ( -0.4332776154273894620, -1.054581703806071857, -1.572814851683856041 ) ) ;
#1879=AXIS2_PLACEMENT_3D ( 'NONE', #1463, #3317, #4430 ) ;
#1882=VERTEX_POINT ( 'NONE', #3873 ) ;
#1883=CARTESIAN_POINT ( 'NONE',  ( 0.4342019027940197673, 0.9783381746514249189, -1.450123259817208687 ) ) ;
#1886=AXIS2_PLACEMENT_3D ( 'NONE', #3173, #6088, #4397 ) ;
#1887=ORIENTED_EDGE ( 'NONE', *, *, #1729, .F. ) ;
#1892=CARTESIAN_POINT ( 'NONE',  ( 1.056523642887408521, -0.5141614760841347609, -1.484898342931014303 ) ) ;
#1894=DIRECTION ( 'NONE',  ( 2.204015539012438360E-32, 4.625929269271482167E-15, -1.000000000000000000 ) ) ;
#1901=CARTESIAN_POINT ( 'NONE',  ( 0.4330708661417323468, -1.051607547633158113, -1.573502280244651441 ) ) ;
#1910=ORIENTED_EDGE ( 'NONE', *, *, #7518, .F. ) ;
#1915=ORIENTED_EDGE ( 'NONE', *, *, #5532, .T. ) ;
#1918=DIRECTION ( 'NONE',  ( -2.312579046053608732E-29, 2.207829878515936732E-15, 1.000000000000000000 ) ) ;
#1924=EDGE_CURVE ( 'NONE', #477, #7296, #4618, .T. ) ;
#1931=EDGE_CURVE ( 'NONE', #5648, #3371, #1075, .T. ) ;
#1936=CARTESIAN_POINT ( 'NONE',  ( -0.4627498550472187722, 0.8884031170519979259, -1.439912866901233324 ) ) ;
#1937=CARTESIAN_POINT ( 'NONE',  ( -0.9044344578135158352, -0.4526814320286502435, -1.447629106959918754 ) ) ;
#1943=DIRECTION ( 'NONE',  ( 5.296894631669315808E-46, -1.000000000000000000, 2.207829878515936732E-15 ) ) ;
#1944=DIRECTION ( 'NONE',  ( -0.000000000000000000, -0.000000000000000000, 1.000000000000000000 ) ) ;
#1947=CARTESIAN_POINT ( 'NONE',  ( -0.9921522615226839870, 0.4406689276647562936, -1.439080857166193717 ) ) ;
#1954=CIRCLE ( 'NONE', #7316, 0.2831409772408586822 ) ;
#1960=CARTESIAN_POINT ( 'NONE',  ( 0.000000000000000000, 0.000000000000000000, -0.7983802283864780414 ) ) ;
#1967=AXIS2_PLACEMENT_3D ( 'NONE', #574, #4493, #6821 ) ;
#1969=ADVANCED_FACE ( 'NONE', ( #4848 ), #4380, .T. ) ;
#1972=VERTEX_POINT ( 'NONE', #1824 ) ;
#1973=AXIS2_PLACEMENT_3D ( 'NONE', #2354, #4769, #3622 ) ;
#1981=CARTESIAN_POINT ( 'NONE',  ( -0.4700904924197908397, 0.8785537298370134085, -1.433776001880364470 ) ) ;
#1983=AXIS2_PLACEMENT_3D ( 'NONE', #7476, #984, #2251 ) ;
#1986=CARTESIAN_POINT ( 'NONE',  ( 0.4330708661417322913, -1.048552902599920289, -1.573978973432616835 ) ) ;
#1991=CARTESIAN_POINT ( 'NONE',  ( -0.4341579107162092943, 1.060348520640341352, -1.570964845243104646 ) ) ;
#1998=CARTESIAN_POINT ( 'NONE',  ( 0.4330708661417320138, 0.9604263920613175243, -1.456063616177414310 ) ) ;
#2004=CARTESIAN_POINT ( 'NONE',  ( 0.8785537298370166281, -0.4700904924197814028, -1.433776001880362250 ) ) ;
#2021=EDGE_CURVE ( 'NONE', #735, #781, #4255, .T. ) ;
#2027=CARTESIAN_POINT ( 'NONE',  ( -0.4619485889667617196, 0.9755734897585889298, -1.553989674004691901 ) ) ;
#2029=CARTESIAN_POINT ( 'NONE',  ( 5.385555596699504477E-15, -0.5141614760841457521, -2.204724409448820754 ) ) ;
#2034=CARTESIAN_POINT ( 'NONE',  ( 0.4996355910473239681, 1.070877566692228999, -1.498503231159224791 ) ) ;
#2037=CARTESIAN_POINT ( 'NONE',  ( 0.4416272204090973541, -1.010074371201533205, -1.570717485485533249 ) ) ;
#2041=CARTESIAN_POINT ( 'NONE',  ( 0.000000000000000000, 0.000000000000000000, -2.204724409448820754 ) ) ;
#2043=CARTESIAN_POINT ( 'NONE',  ( -1.041228047528456102, 0.4333661275892043419, -1.574803149606299302 ) ) ;
#2044=CARTESIAN_POINT ( 'NONE',  ( -5.154746071126634886E-15, 0.4921259842519648542, -2.204724409448822975 ) ) ;
#2045=VERTEX_POINT ( 'NONE', #5348 ) ;
#2054=CARTESIAN_POINT ( 'NONE',  ( 1.056523642887397862, 0.5141614760841569653, -1.484898342931014303 ) ) ;
#2056=CARTESIAN_POINT ( 'NONE',  ( -0.9221073153504516506, -0.4437903857718360490, -1.453484209829405849 ) ) ;
#2057=CIRCLE ( 'NONE', #4007, 1.043121362164705745 ) ;
#2063=CARTESIAN_POINT ( 'NONE',  ( 0.9752011746067855702, -0.4617902729109746307, -1.554226146212451809 ) ) ;
#2065=CARTESIAN_POINT ( 'NONE',  ( -0.9990286922241471412, 0.4596433552321222415, -1.415369843883346412 ) ) ;
#2081=CARTESIAN_POINT ( 'NONE',  ( 0.9990286721055757768, 0.4596436929058995702, -1.415369458146015447 ) ) ;
#2086=ORIENTED_EDGE ( 'NONE', *, *, #1200, .T. ) ;
#2089=VERTEX_POINT ( 'NONE', #2592 ) ;
#2094=AXIS2_PLACEMENT_3D ( 'NONE', #2537, #822, #6070 ) ;
#2095=CARTESIAN_POINT ( 'NONE',  ( 0.4330708661417322913, 1.044891351410287994, -1.574550377471545692 ) ) ;
#2097=AXIS2_PLACEMENT_3D ( 'NONE', #2109, #3787, #6120 ) ;
#2104=SHAPE_REPRESENTATION ( 'MAT-019 Puller', ( #5166 ), #7344 ) ;
#2109=CARTESIAN_POINT ( 'NONE',  ( 0.000000000000000000, 0.000000000000000000, -2.204724409448820754 ) ) ;
#2113=CARTESIAN_POINT ( 'NONE',  ( -0.4342018836190598141, -0.9783380834473016652, -1.450123305573145283 ) ) ;
#2116=EDGE_CURVE ( 'NONE', #3650, #6826, #6159, .T. ) ;
#2118=ORIENTED_EDGE ( 'NONE', *, *, #3754, .T. ) ;
#2121=LENGTH_MEASURE_WITH_UNIT ( LENGTH_MEASURE( 0.02539999999999999897 ), #3727 );
#2134=DIRECTION ( 'NONE',  ( 0.000000000000000000, 0.000000000000000000, 1.000000000000000000 ) ) ;
#2141=CARTESIAN_POINT ( 'NONE',  ( 0.9666437042230172638, -0.4330708661417221883, -1.454455828411335583 ) ) ;
#2142=B_SPLINE_CURVE_WITH_KNOTS ( 'NONE', 3,
 ( #4967, #2591, #837, #7324, #3858, #985, #1431, #950, #6722, #3781 ),
 .UNSPECIFIED., .F., .F.,
 ( 4, 2, 2, 2, 4 ),
 ( 3.469446951953614189E-18, 0.0005494620090385992067, 0.001098924018077194944, 0.001648386027115790681, 0.002197848036154386418 ),
 .UNSPECIFIED. ) ;
#2144=VERTEX_POINT ( 'NONE', #227 ) ;
#2146=CARTESIAN_POINT ( 'NONE',  ( -1.056523642887404968, 0.5141614760841421994, -1.484898342931014525 ) ) ;
#2148=EDGE_LOOP ( 'NONE', ( #1753, #6361 ) ) ;
#2158=CARTESIAN_POINT ( 'NONE',  ( -0.4330708661417317362, 1.048552902599920733, -1.573978973432617279 ) ) ;
#2159=ORIENTED_EDGE ( 'NONE', *, *, #7058, .T. ) ;
#2164=CARTESIAN_POINT ( 'NONE',  ( -0.9346850374427957409, 0.4388996395293537911, -1.455943645409046638 ) ) ;
#2169=DIRECTION ( 'NONE',  ( 1.000000000000000000, 0.000000000000000000, -0.000000000000000000 ) ) ;
#2172=CARTESIAN_POINT ( 'NONE',  ( 0.4437902010346556625, 0.9221077491748230770, -1.453484313640521552 ) ) ;
#2177=ORIENTED_EDGE ( 'NONE', *, *, #7461, .T. ) ;
#2178=CARTESIAN_POINT ( 'NONE',  ( 0.4406689276647596243, -0.9921522615226822106, -1.439080857166193939 ) ) ;
#2181=CARTESIAN_POINT ( 'NONE',  ( -0.5141614760841421994, 0.000000000000000000, -2.204724409448823419 ) ) ;
#2182=ORIENTED_EDGE ( 'NONE', *, *, #298, .T. ) ;
#2199=EDGE_CURVE ( 'NONE', #3405, #3650, #4011, .T. ) ;
#2203=DIRECTION ( 'NONE',  ( 1.000000000000000000, 0.000000000000000000, 2.207829878515936732E-15 ) ) ;
#2209=CARTESIAN_POINT ( 'NONE',  ( 0.000000000000000000, 0.000000000000000000, -0.8561751947315059397 ) ) ;
#2214=VERTEX_POINT ( 'NONE', #6028 ) ;
#2218=CARTESIAN_POINT ( 'NONE',  ( 0.000000000000000000, 0.000000000000000000, -3.582716535433073002 ) ) ;
#2219=DIRECTION ( 'NONE',  ( -0.000000000000000000, -0.000000000000000000, 1.000000000000000000 ) ) ;
#2221=FACE_OUTER_BOUND ( 'NONE', #2563, .T. ) ;
#2230=CARTESIAN_POINT ( 'NONE',  ( -0.4339190921229451603, 0.9541934910893049571, -1.456692913385828847 ) ) ;
#2232=CARTESIAN_POINT ( 'NONE',  ( 1.089828288828796898, -1.334654725534422735E-16, -1.361499588670820771 ) ) ;
#2237=EDGE_LOOP ( 'NONE', ( #2579, #6388, #6195, #6601 ) ) ;
#2244=CARTESIAN_POINT ( 'NONE',  ( -0.9666437042230129340, -0.4330708661417356220, -1.454455828411337359 ) ) ;
#2246=EDGE_CURVE ( 'NONE', #3292, #6423, #1304, .T. ) ;
#2251=DIRECTION ( 'NONE',  ( -4.625929269271482167E-15, 0.000000000000000000, 1.000000000000000000 ) ) ;
#2252=EDGE_CURVE ( 'NONE', #3756, #1492, #6792, .T. ) ;
#2253=DIRECTION ( 'NONE',  ( -1.000000000000000000, 0.000000000000000000, -2.193342766891361226E-15 ) ) ;
#2258=CARTESIAN_POINT ( 'NONE',  ( -0.9867938558989102216, -0.4882975260543767071, -1.385219839936553177 ) ) ;
#2267=CARTESIAN_POINT ( 'NONE',  ( 0.9666437042230099363, 0.4330708661417423944, -1.454455828411337359 ) ) ;
#2282=DIRECTION ( 'NONE',  ( -1.000000000000000000, 0.000000000000000000, 0.000000000000000000 ) ) ;
#2285=EDGE_CURVE ( 'NONE', #345, #7028, #243, .T. ) ;
#2286=CARTESIAN_POINT ( 'NONE',  ( -0.4999740374263542675, -0.9773781006402580962, -1.373989084484001477 ) ) ;
#2287=B_SPLINE_CURVE_WITH_KNOTS ( 'NONE', 3,
 ( #6766, #277, #2558, #2598 ),
 .UNSPECIFIED., .F., .F.,
 ( 4, 4 ),
 ( 6.938893903907228378E-18, 0.0002807012396509452013 ),
 .UNSPECIFIED. ) ;
#2290=VERTEX_POINT ( 'NONE', #1644 ) ;
#2306=CARTESIAN_POINT ( 'NONE',  ( 0.9221077491748198574, 0.4437902010346655435, -1.453484313640523107 ) ) ;
#2319=CARTESIAN_POINT ( 'NONE',  ( -0.4508656291625802726, -1.083410641227605886, -1.549345754620972349 ) ) ;
#2323=CIRCLE ( 'NONE', #2456, 1.168853328413307358 ) ;
#2327=VERTEX_POINT ( 'NONE', #6383 ) ;
#2329=CARTESIAN_POINT ( 'NONE',  ( -1.866451592287363150E-29, 1.781909941321919274E-15, -1.397637795275591843 ) ) ;
#2332=AXIS2_PLACEMENT_3D ( 'NONE', #1960, #6631, #4291 ) ;
#2333=CARTESIAN_POINT ( 'NONE',  ( -1.030265555772312824, 0.4349482935633047220, -1.574803149606299302 ) ) ;
#2337=AXIS2_PLACEMENT_3D ( 'NONE', #1835, #4249, #3639 ) ;
#2343=AXIS2_PLACEMENT_3D ( 'NONE', #1445, #5599, #886 ) ;
#2346=EDGE_LOOP ( 'NONE', ( #391, #7371, #3826, #576, #3602, #248 ) ) ;
#2350=DIRECTION ( 'NONE',  ( 0.000000000000000000, 1.000000000000000000, 2.193342766891360832E-15 ) ) ;
#2352=CARTESIAN_POINT ( 'NONE',  ( -0.4541662050560832387, -0.9857970000181586201, -1.560880783937515170 ) ) ;
#2353=CARTESIAN_POINT ( 'NONE',  ( 0.9666437042230099363, 0.4330708661417423944, -1.454455828411337359 ) ) ;
#2354=CARTESIAN_POINT ( 'NONE',  ( 0.000000000000000000, 0.000000000000000000, 0.000000000000000000 ) ) ;
#2355=DIRECTION ( 'NONE',  ( -2.312579046053608732E-29, 2.207829878515936732E-15, 1.000000000000000000 ) ) ;
#2358=CARTESIAN_POINT ( 'NONE',  ( -0.4403524516313984116, -1.075169953371343023, -1.561970681382796045 ) ) ;
#2362=AXIS2_PLACEMENT_3D ( 'NONE', #451, #6043, #4314 ) ;
#2377=CARTESIAN_POINT ( 'NONE',  ( -1.081428632361001396, -0.4470329974975803533, -1.553789141944099450 ) ) ;
#2378=ADVANCED_FACE ( 'NONE', ( #3820 ), #2663, .T. ) ;
#2379=DIRECTION ( 'NONE',  ( -1.000000000000000000, -0.000000000000000000, -4.625929269271482167E-15 ) ) ;
#2386=DIRECTION ( 'NONE',  ( -7.708596820178695308E-30, 2.207829878515936732E-15, -1.000000000000000000 ) ) ;
#2388=EDGE_CURVE ( 'NONE', #6137, #3685, #6703, .T. ) ;
#2391=CARTESIAN_POINT ( 'NONE',  ( -0.4514965799695756510, 0.9983959133492268379, -1.424958590981962203 ) ) ;
#2395=CARTESIAN_POINT ( 'NONE',  ( -0.5073440712900673111, -0.9696655408444068147, -1.367310953805448426 ) ) ;
#2398=EDGE_LOOP ( 'NONE', ( #6597, #1227, #7274, #1653 ) ) ;
#2405=DIRECTION ( 'NONE',  ( -3.491481338843133750E-15, 1.000000000000000000, 0.000000000000000000 ) ) ;
#2407=CARTESIAN_POINT ( 'NONE',  ( 0.4720891361949481890, 0.9960021845704859489, -1.401719468380311362 ) ) ;
#2427=CARTESIAN_POINT ( 'NONE',  ( -1.085572738833922246, 0.4589124540220903548, -1.540322878613943125 ) ) ;
#2435=CARTESIAN_POINT ( 'NONE',  ( 0.4700904924197906176, -0.8785537298370117432, -1.433776001880362250 ) ) ;
#2436=CARTESIAN_POINT ( 'NONE',  ( -1.044891351410288660, -0.4330708661417352334, -1.574550377471545470 ) ) ;
#2437=CARTESIAN_POINT ( 'NONE',  ( 1.056523642887397862, 0.5141614760841569653, -1.484898342931014303 ) ) ;
#2444=CARTESIAN_POINT ( 'NONE',  ( -0.4713813068963899067, -1.084813395429188088, -1.526966363676886873 ) ) ;
#2445=CARTESIAN_POINT ( 'NONE',  ( 1.048552902599916292, 0.4330708661417427274, -1.573978973432617279 ) ) ;
#2448=ORIENTED_EDGE ( 'NONE', *, *, #5803, .T. ) ;
#2449=CARTESIAN_POINT ( 'NONE',  ( 0.5141614760841460852, 0.9609181420092316461, -1.361499588670819216 ) ) ;
#2456=AXIS2_PLACEMENT_3D ( 'NONE', #1775, #3007, #1740 ) ;
#2458=FACE_OUTER_BOUND ( 'NONE', #5570, .T. ) ;
#2462=DIRECTION ( 'NONE',  ( 3.491481338843133750E-15, -1.000000000000000000, -4.625929269271482167E-15 ) ) ;
#2465=B_SPLINE_CURVE_WITH_KNOTS ( 'NONE', 3,
 ( #2857, #2786, #1599, #2141 ),
 .UNSPECIFIED., .F., .F.,
 ( 4, 4 ),
 ( 0.000000000000000000, 0.0004815725036528544921 ),
 .UNSPECIFIED. ) ;
#2469=CARTESIAN_POINT ( 'NONE',  ( 0.4353079511162236126, 0.9479499796399308842, -1.456692913385826849 ) ) ;
#2470=AXIS2_PLACEMENT_3D ( 'NONE', #2329, #1918, #7120 ) ;
#2475=CARTESIAN_POINT ( 'NONE',  ( 0.4353079511162236126, -0.9479499796399308842, -1.456692913385826849 ) ) ;
#2476=CARTESIAN_POINT ( 'NONE',  ( -0.4720891361949479115, 0.9960021845704875032, -1.401719468380313360 ) ) ;
#2477=DIRECTION ( 'NONE',  ( 4.615976749461841764E-15, 0.000000000000000000, -1.000000000000000000 ) ) ;
#2494=ORIENTED_EDGE ( 'NONE', *, *, #246, .F. ) ;
#2501=ORIENTED_EDGE ( 'NONE', *, *, #4496, .T. ) ;
#2504=CARTESIAN_POINT ( 'NONE',  ( -0.4338950423154138147, -1.037563309807725043, -1.574803149606299302 ) ) ;
#2507=CARTESIAN_POINT ( 'NONE',  ( -1.070856827570680903, 0.4375700189966262865, -1.565644132322242532 ) ) ;
#2509=DIRECTION ( 'NONE',  ( -4.625929269271482167E-15, 0.000000000000000000, 1.000000000000000000 ) ) ;
#2510=CARTESIAN_POINT ( 'NONE',  ( -1.651526287078852914E-15, 0.000000000000000000, -1.456692913385827515 ) ) ;
#2511=CARTESIAN_POINT ( 'NONE',  ( 1.085749034841576810, 0.4630671888207514852, -1.535808138920396138 ) ) ;
#2518=CARTESIAN_POINT ( 'NONE',  ( -0.9696655408442725887, 0.5073440712894341509, -1.367310953804909079 ) ) ;
#2519=CARTESIAN_POINT ( 'NONE',  ( -0.4353079511162236681, 0.9479499796399324385, -1.456692913385828625 ) ) ;
#2530=EDGE_CURVE ( 'NONE', #7296, #3756, #1569, .T. ) ;
#2531=ADVANCED_FACE ( 'NONE', ( #112 ), #1192, .T. ) ;
#2537=CARTESIAN_POINT ( 'NONE',  ( -1.950024051643512521E-29, 1.861696953619914682E-15, -1.361499588670820771 ) ) ;
#2542=CARTESIAN_POINT ( 'NONE',  ( -1.063161251382700234, 0.4348450093584623755, -1.569784523562343770 ) ) ;
#2544=CARTESIAN_POINT ( 'NONE',  ( 0.4403524516313990222, -1.075169953371342801, -1.561970681382796045 ) ) ;
#2547=AXIS2_PLACEMENT_3D ( 'NONE', #1869, #3626, #4817 ) ;
#2552=DIRECTION ( 'NONE',  ( -1.000000000000000000, -1.045898529308444144E-14, 0.000000000000000000 ) ) ;
#2557=CARTESIAN_POINT ( 'NONE',  ( -1.037563309807723488, -0.4338950423154175340, -1.574803149606299302 ) ) ;
#2558=CARTESIAN_POINT ( 'NONE',  ( -0.4333661275892074505, -1.041228047528454770, -1.574803149606299302 ) ) ;
#2561=ADVANCED_FACE ( 'NONE', ( #4774 ), #3524, .T. ) ;
#2563=EDGE_LOOP ( 'NONE', ( #1887, #4363, #863, #619, #586, #5239 ) ) ;
#2568=EDGE_CURVE ( 'NONE', #5974, #5935, #5244, .T. ) ;
#2576=ADVANCED_BREP_SHAPE_REPRESENTATION ( '', ( #4033, #5166 ), #7344 ) ;
#2577=CARTESIAN_POINT ( 'NONE',  ( -0.2952755905511811885, 0.000000000000000000, -0.7983802283864783744 ) ) ;
#2578=EDGE_CURVE ( 'NONE', #811, #443, #2142, .T. ) ;
#2579=ORIENTED_EDGE ( 'NONE', *, *, #5791, .T. ) ;
#2580=AXIS2_PLACEMENT_3D ( 'NONE', #4280, #7331, #4937 ) ;
#2584=CARTESIAN_POINT ( 'NONE',  ( -0.9346848099469026172, -0.4388997119412576531, -1.455943619906243436 ) ) ;
#2587=AXIS2_PLACEMENT_3D ( 'NONE', #5875, #27, #4685 ) ;
#2591=CARTESIAN_POINT ( 'NONE',  ( 1.030265555772306829, 0.4349482935633184333, -1.574803149606299302 ) ) ;
#2592=CARTESIAN_POINT ( 'NONE',  ( -0.8785537298370117432, -0.4700904924197938373, -1.433776001880364470 ) ) ;
#2595=CARTESIAN_POINT ( 'NONE',  ( -0.4756000659977974721, 1.083679028610380346, -1.522578585053779410 ) ) ;
#2598=CARTESIAN_POINT ( 'NONE',  ( -0.4338950423154138147, -1.037563309807725043, -1.574803149606299302 ) ) ;
#2603=CARTESIAN_POINT ( 'NONE',  ( 0.4349482548737268472, -1.030265823844198625, -1.574803149606299524 ) ) ;
#2610=CARTESIAN_POINT ( 'NONE',  ( 1.083410700381150393, -0.4508657589754589967, -1.549345605342071774 ) ) ;
#2612=ORIENTED_EDGE ( 'NONE', *, *, #7191, .F. ) ;
#2613=CLOSED_SHELL ( 'NONE', ( #441, #200, #5016, #7105, #9, #807, #2378, #3180, #4762, #2624, #2561, #5521, #201, #6275, #1585, #2838, #6000, #3930, #4529, #5195, #6970, #6684, #6592, #156, #6880, #5060, #1716, #5330, #3464, #1723, #440, #5199, #2531, #525, #1969, #3840, #6402, #4875, #893, #6683, #377 ) ) ;
#2615=EDGE_CURVE ( 'NONE', #7028, #4474, #4135, .T. ) ;
#2620=EDGE_CURVE ( 'NONE', #1688, #7237, #3162, .T. ) ;
#2624=ADVANCED_FACE ( 'NONE', ( #6082 ), #849, .T. ) ;
#2627=CARTESIAN_POINT ( 'NONE',  ( 1.048552902599924730, -0.4330708661417213001, -1.573978973432616835 ) ) ;
#2630=CARTESIAN_POINT ( 'NONE',  ( -0.9726683636255533116, 0.4332839536939371294, -1.452651081959918766 ) ) ;
#2642=ORIENTED_EDGE ( 'NONE', *, *, #3467, .T. ) ;
#2645=CARTESIAN_POINT ( 'NONE',  ( 0.9696319393320019797, -0.5073702590894858533, -1.367288630523686210 ) ) ;
#2659=DIRECTION ( 'NONE',  ( 0.000000000000000000, -1.000000000000000000, -2.095133389269358970E-15 ) ) ;
#2663=CYLINDRICAL_SURFACE ( 'NONE', #4743, 0.2362204724409449341 ) ;
#2666=EDGE_CURVE ( 'NONE', #2214, #283, #5528, .T. ) ;
#2673=CARTESIAN_POINT ( 'NONE',  ( -0.9783380834473003329, -0.4342018836190635334, -1.450123305573145505 ) ) ;
#2680=DIRECTION ( 'NONE',  ( 1.000000000000000000, 0.000000000000000000, 0.000000000000000000 ) ) ;
#2682=CARTESIAN_POINT ( 'NONE',  ( -1.044891351410289548, 0.4330708661417286276, -1.574550377471545692 ) ) ;
#2686=DIRECTION ( 'NONE',  ( -3.491481338843133750E-15, 1.000000000000000000, 0.000000000000000000 ) ) ;
#2690=ORIENTED_EDGE ( 'NONE', *, *, #246, .T. ) ;
#2692=CARTESIAN_POINT ( 'NONE',  ( -0.4921259842519648542, 0.000000000000000000, -2.204724409448822975 ) ) ;
#2699=CIRCLE ( 'NONE', #5999, 1.089828288828796676 ) ;
#2703=AXIS2_PLACEMENT_3D ( 'NONE', #1237, #3586, #2477 ) ;
#2709=ORIENTED_EDGE ( 'NONE', *, *, #4538, .T. ) ;
#2711=EDGE_CURVE ( 'NONE', #4601, #5274, #1803, .T. ) ;
#2716=CARTESIAN_POINT ( 'NONE',  ( -0.9810555383103370941, -0.4349192646538896367, -1.448591292758283799 ) ) ;
#2717=EDGE_LOOP ( 'NONE', ( #5204, #7489, #44, #6736, #1007, #291 ) ) ;
#2719=CARTESIAN_POINT ( 'NONE',  ( 1.051607560569809863, -0.4330708661417213001, -1.573502278225820561 ) ) ;
#2726=CARTESIAN_POINT ( 'NONE',  ( -0.4330708661417322913, 0.9604263920613194117, -1.456063616177416087 ) ) ;
#2727=DIRECTION ( 'NONE',  ( -0.000000000000000000, -0.000000000000000000, 1.000000000000000000 ) ) ;
#2732=VERTEX_POINT ( 'NONE', #4093 ) ;
#2741=DIRECTION ( 'NONE',  ( 1.000000000000000000, 0.000000000000000000, 0.000000000000000000 ) ) ;
#2751=ORIENTED_EDGE ( 'NONE', *, *, #4435, .F. ) ;
#2774=DIRECTION ( 'NONE',  ( -2.207829878515936732E-15, 0.000000000000000000, 1.000000000000000000 ) ) ;
#2783=DIRECTION ( 'NONE',  ( 1.000000000000000000, 0.000000000000000000, 2.207829878515936732E-15 ) ) ;
#2784=ORIENTED_EDGE ( 'NONE', *, *, #1146, .T. ) ;
#2785=CARTESIAN_POINT ( 'NONE',  ( 0.4342018836190599251, -0.9783380834472997778, -1.450123305573142840 ) ) ;
#2786=CARTESIAN_POINT ( 'NONE',  ( 0.9541934910893076216, -0.4339190921229351683, -1.456692913385826849 ) ) ;
#2789=DIRECTION ( 'NONE',  ( -4.625929269271482167E-15, 0.000000000000000000, 1.000000000000000000 ) ) ;
#2790=ORIENTED_EDGE ( 'NONE', *, *, #5803, .F. ) ;
#2817=DIRECTION ( 'NONE',  ( 1.765631543889772066E-46, -1.000000000000000000, -2.207829878515936732E-15 ) ) ;
#2822=ORIENTED_EDGE ( 'NONE', *, *, #6180, .F. ) ;
#2828=AXIS2_PLACEMENT_3D ( 'NONE', #1713, #6389, #2897 ) ;
#2833=DIRECTION ( 'NONE',  ( -1.000000000000000000, -8.881784197001252323E-16, 0.000000000000000000 ) ) ;
#2836=EDGE_LOOP ( 'NONE', ( #955, #6067, #5406, #3912 ) ) ;
#2838=ADVANCED_FACE ( 'NONE', ( #5099 ), #6339, .T. ) ;
#2847=EDGE_CURVE ( 'NONE', #4601, #4341, #5779, .T. ) ;
#2853=CARTESIAN_POINT ( 'NONE',  ( 0.000000000000000000, 0.000000000000000000, -1.546597720061111847 ) ) ;
#2854=EDGE_CURVE ( 'NONE', #3405, #4833, #3026, .T. ) ;
#2855=EDGE_CURVE ( 'NONE', #1409, #269, #1031, .T. ) ;
#2856=TOROIDAL_SURFACE ( 'NONE', #1025, 1.043121362164705745, 0.05905511811023622659 ) ;
#2857=CARTESIAN_POINT ( 'NONE',  ( 0.9479499796399352141, -0.4353079511162137316, -1.456692913385826849 ) ) ;
#2861=CARTESIAN_POINT ( 'NONE',  ( 1.048552902599924730, -0.4330708661417213001, -1.573978973432616835 ) ) ;
#2870=DIRECTION ( 'NONE',  ( 0.000000000000000000, 0.000000000000000000, 1.000000000000000000 ) ) ;
#2887=EDGE_CURVE ( 'NONE', #3371, #4601, #3224, .T. ) ;
#2888=CARTESIAN_POINT ( 'NONE',  ( -0.4596433552321257388, -0.9990286922241469192, -1.415369843883347967 ) ) ;
#2889=EDGE_LOOP ( 'NONE', ( #4520, #888, #71, #6177, #3870, #6327 ) ) ;
#2891=EDGE_CURVE ( 'NONE', #4488, #3292, #1578, .T. ) ;
#2896=ORIENTED_EDGE ( 'NONE', *, *, #4347, .F. ) ;
#2897=DIRECTION ( 'NONE',  ( 1.000000000000000000, 0.000000000000000000, 0.000000000000000000 ) ) ;
#2903=ORIENTED_EDGE ( 'NONE', *, *, #4615, .T. ) ;
#2921=DIRECTION ( 'NONE',  ( 0.000000000000000000, 4.632546475182561102E-15, -1.000000000000000000 ) ) ;
#2922=CARTESIAN_POINT ( 'NONE',  ( -1.048552902599919401, -0.4330708661417353444, -1.573978973432617279 ) ) ;
#2924=CARTESIAN_POINT ( 'NONE',  ( -0.4637690556582350077, -0.9984401429152556240, -1.410743228759551604 ) ) ;
#2931=CIRCLE ( 'NONE', #3682, 0.2362204724409449341 ) ;
#2940=CARTESIAN_POINT ( 'NONE',  ( -0.9705345056685864558, 0.4659838021920478246, -1.550372027848833545 ) ) ;
#2941=EDGE_CURVE ( 'NONE', #3522, #75, #5147, .T. ) ;
#2943=AXIS2_PLACEMENT_3D ( 'NONE', #6374, #2386, #2350 ) ;
#2944=DIRECTION ( 'NONE',  ( 2.312579046053608732E-29, -2.207829878515936732E-15, -1.000000000000000000 ) ) ;
#2950=CARTESIAN_POINT ( 'NONE',  ( -0.4330708661417287941, 0.000000000000000000, -2.204724409448822975 ) ) ;
#2952=CIRCLE ( 'NONE', #5670, 1.223643328182682621 ) ;
#2958=FACE_OUTER_BOUND ( 'NONE', #5317, .T. ) ;
#2963=CARTESIAN_POINT ( 'NONE',  ( 0.9697097892794885876, 0.4330708661417424499, -1.453662943332487023 ) ) ;
#2972=CARTESIAN_POINT ( 'NONE',  ( -0.4589124540220937964, -1.085572738833920248, -1.540322878613942681 ) ) ;
#2975=ORIENTED_EDGE ( 'NONE', *, *, #287, .F. ) ;
#2989=EDGE_CURVE ( 'NONE', #5974, #5274, #7227, .T. ) ;
#2990=CARTESIAN_POINT ( 'NONE',  ( -1.037563309807726375, 0.4338950423154108171, -1.574803149606299302 ) ) ;
#2993=DIRECTION ( 'NONE',  ( -4.632546475182562680E-15, 0.000000000000000000, 1.000000000000000000 ) ) ;
#3002=DIRECTION ( 'NONE',  ( 1.047444401652940007E-14, -1.000000000000000000, 0.000000000000000000 ) ) ;
#3006=CARTESIAN_POINT ( 'NONE',  ( -0.4596436929058889120, 0.9990286721055804398, -1.415369458146015447 ) ) ;
#3007=DIRECTION ( 'NONE',  ( 3.491481338843133750E-15, -1.000000000000000000, -0.000000000000000000 ) ) ;
#3010=CARTESIAN_POINT ( 'NONE',  ( -0.4762522394722485397, -0.9941399105654894486, -1.397361772547375480 ) ) ;
#3011=ORIENTED_EDGE ( 'NONE', *, *, #7285, .T. ) ;
#3012=CARTESIAN_POINT ( 'NONE',  ( 0.5141614760841460852, 0.9609181420092316461, -1.361499588670819216 ) ) ;
#3013=DIRECTION ( 'NONE',  ( 0.000000000000000000, 0.000000000000000000, -1.000000000000000000 ) ) ;
#3019=ORIENTED_EDGE ( 'NONE', *, *, #6223, .F. ) ;
#3026=B_SPLINE_CURVE_WITH_KNOTS ( 'NONE', 3,
 ( #6814, #5142, #1568, #3219, #4983, #7301, #6779, #5567, #2081, #3916, #6244, #1003, #3338, #5341, #4196, #6535, #2963, #2353 ),
 .UNSPECIFIED., .F., .F.,
 ( 4, 2, 2, 2, 2, 2, 2, 2, 4 ),
 ( -8.121667112571881724E-06, 0.0009422843086939815564, 0.001417487296597250493, 0.001892690284500519538, 0.002367893272403787715, 0.002843096260307056544, 0.003318299248210325372, 0.003555900742161956316, 0.003793502236113587694 ),
 .UNSPECIFIED. ) ;
#3030=CARTESIAN_POINT ( 'NONE',  ( 0.4921259842519683514, 0.000000000000000000, -2.204724409448820754 ) ) ;
#3031=VERTEX_POINT ( 'NONE', #2504 ) ;
#3032=DIRECTION ( 'NONE',  ( -0.000000000000000000, -1.000000000000000000, -0.000000000000000000 ) ) ;
#3037=CARTESIAN_POINT ( 'NONE',  ( -1.064268091466843202, 0.5072022184699304104, -1.491294347566136436 ) ) ;
#3042=CARTESIAN_POINT ( 'NONE',  ( -0.4338950423154138147, -1.037563309807725043, -1.574803149606299302 ) ) ;
#3043=CARTESIAN_POINT ( 'NONE',  ( -0.4843361811957747065, 0.9895437626941984144, -1.389133361342960393 ) ) ;
#3053=CARTESIAN_POINT ( 'NONE',  ( -1.512058847530491023E-15, 0.4330708661417322913, -2.204724409448820754 ) ) ;
#3058=ORIENTED_EDGE ( 'NONE', *, *, #1931, .F. ) ;
#3069=CARTESIAN_POINT ( 'NONE',  ( -1.064268091467049926, -0.5072022184714435333, -1.491294347567520218 ) ) ;
#3075=CARTESIAN_POINT ( 'NONE',  ( -0.4663632139997256898, 0.8833361873720764201, -1.436953241411954130 ) ) ;
#3084=CARTESIAN_POINT ( 'NONE',  ( 0.4333661275892079501, 1.041228047528454548, -1.574803149606299302 ) ) ;
#3106=ORIENTED_EDGE ( 'NONE', *, *, #5532, .F. ) ;
#3108=ORIENTED_EDGE ( 'NONE', *, *, #5383, .T. ) ;
#3113=B_SPLINE_CURVE_WITH_KNOTS ( 'NONE', 3,
 ( #147, #6039, #7280, #6110, #1937, #185, #2056, #2584, #4385, #1460 ),
 .UNSPECIFIED., .F., .F.,
 ( 4, 2, 2, 2, 4 ),
 ( -7.765797721861150373E-06, 0.0005114169989440397893, 0.001030599795609940875, 0.001549782592275841852, 0.002068965388941742829 ),
 .UNSPECIFIED. ) ;
#3122=CARTESIAN_POINT ( 'NONE',  ( 0.4338950423154144254, -1.037563309807725043, -1.574803149606299302 ) ) ;
#3124=CARTESIAN_POINT ( 'NONE',  ( 4.923936545553833138E-15, -0.4700904924197903956, -2.204724409448820754 ) ) ;
#3125=ORIENTED_EDGE ( 'NONE', *, *, #7330, .T. ) ;
#3135=CARTESIAN_POINT ( 'NONE',  ( -1.048552902599921843, 0.4330708661417285721, -1.573978973432616835 ) ) ;
#3139=ORIENTED_EDGE ( 'NONE', *, *, #2116, .F. ) ;
#3153=ORIENTED_EDGE ( 'NONE', *, *, #1626, .F. ) ;
#3159=CARTESIAN_POINT ( 'NONE',  ( 0.4470329974975768006, -1.081428632361001840, -1.553789141944100338 ) ) ;
#3162=CIRCLE ( 'NONE', #7433, 1.259842519685039353 ) ;
#3166=DIRECTION ( 'NONE',  ( 0.000000000000000000, 1.000000000000000000, 0.000000000000000000 ) ) ;
#3168=ORIENTED_EDGE ( 'NONE', *, *, #6492, .F. ) ;
#3169=CARTESIAN_POINT ( 'NONE',  ( -0.9983958463931813521, 0.4514963146295044027, -1.424958914991360182 ) ) ;
#3173=CARTESIAN_POINT ( 'NONE',  ( 0.000000000000000000, 0.000000000000000000, -2.204724409448820754 ) ) ;
#3179=B_SPLINE_CURVE_WITH_KNOTS ( 'NONE', 3,
 ( #6918, #3985, #6311, #2113, #4013, #6344, #3440, #6952, #4653, #2888, #2924, #3508, #3010, #1706, #5346, #2286, #2395, #4048 ),
 .UNSPECIFIED., .F., .F.,
 ( 4, 2, 2, 2, 2, 2, 2, 2, 4 ),
 ( 0.000000000000000000, 0.0002385177155853689210, 0.0004770354311707378421, 0.0009540708623414871766, 0.001431106293512236349, 0.001908141724682985629, 0.002385177155853734909, 0.002862212587024484407, 0.003816283449365995978 ),
 .UNSPECIFIED. ) ;
#3180=ADVANCED_FACE ( 'NONE', ( #5860 ), #3521, .T. ) ;
#3184=EDGE_CURVE ( 'NONE', #1691, #709, #4862, .T. ) ;
#3186=DIRECTION ( 'NONE',  ( -1.047444401652940007E-14, 1.000000000000000000, -4.625929269271482167E-15 ) ) ;
#3198=CIRCLE ( 'NONE', #4171, 1.124634398195722973 ) ;
#3200=B_SPLINE_CURVE_WITH_KNOTS ( 'NONE', 3,
 ( #2519, #6619, #788, #100, #1806, #4838, #7052, #1936, #3075, #4266 ),
 .UNSPECIFIED., .F., .F.,
 ( 4, 2, 2, 2, 4 ),
 ( 0.000000000000000000, 0.0005216184974661253193, 0.001043236994932250639, 0.001564855492398375958, 0.002086473989864501277 ),
 .UNSPECIFIED. ) ;
#3205=EDGE_LOOP ( 'NONE', ( #3372, #4901, #6666, #4458, #6635, #6524 ) ) ;
#3208=CIRCLE ( 'NONE', #1120, 1.223643328182681511 ) ;
#3212=CARTESIAN_POINT ( 'NONE',  ( 0.4630671888207407161, 1.085749034841581695, -1.535808138920397026 ) ) ;
#3214=CARTESIAN_POINT ( 'NONE',  ( -0.9479499796399322165, 0.4353079511162203374, -1.456692913385826849 ) ) ;
#3219=CARTESIAN_POINT ( 'NONE',  ( 0.9867934559254182281, 0.4882980771758929639, -1.385219299502222556 ) ) ;
#3224=B_SPLINE_CURVE_WITH_KNOTS ( 'NONE', 3,
 ( #4812, #65, #5880, #642, #3043, #4727, #2476, #5305, #3006, #2391, #5385, #1774, #1157, #106, #3585, #3505, #5841, #4768 ),
 .UNSPECIFIED., .F., .F.,
 ( 4, 2, 2, 2, 2, 2, 2, 2, 4 ),
 ( -8.121667112564153395E-06, 0.0009422843086939946752, 0.001417487296597265889, 0.001892690284500537319, 0.002367893272403808966, 0.002843096260307079962, 0.003318299248210351392, 0.003555900742161983638, 0.003793502236113614583 ),
 .UNSPECIFIED. ) ;
#3226=ORIENTED_EDGE ( 'NONE', *, *, #2887, .T. ) ;
#3236=DIRECTION ( 'NONE',  ( -0.000000000000000000, -0.000000000000000000, 1.000000000000000000 ) ) ;
#3239=CARTESIAN_POINT ( 'NONE',  ( 0.9044344578135206092, -0.4526814320286376425, -1.447629106959917200 ) ) ;
#3246=CARTESIAN_POINT ( 'NONE',  ( 0.4878048847236821084, 1.078368654584403785, -1.510181419419387439 ) ) ;
#3250=ORIENTED_EDGE ( 'NONE', *, *, #2855, .F. ) ;
#3252=VERTEX_POINT ( 'NONE', #3562 ) ;
#3253=CARTESIAN_POINT ( 'NONE',  ( 1.037563309807720380, 0.4338950423154246394, -1.574803149606299302 ) ) ;
#3258=CARTESIAN_POINT ( 'NONE',  ( 0.9773775067402716843, -0.4999746636856364779, -1.373988502838978665 ) ) ;
#3259=ORIENTED_EDGE ( 'NONE', *, *, #7229, .T. ) ;
#3271=EDGE_CURVE ( 'NONE', #5720, #269, #938, .T. ) ;
#3272=CIRCLE ( 'NONE', #476, 1.043121362164705745 ) ;
#3274=CARTESIAN_POINT ( 'NONE',  ( 0.4466261709646375810, 0.9159932075028739407, -1.451746187131333521 ) ) ;
#3275=AXIS2_PLACEMENT_3D ( 'NONE', #3030, #4223, #6561 ) ;
#3276=DIRECTION ( 'NONE',  ( 1.000000000000000000, 0.000000000000000000, 0.000000000000000000 ) ) ;
#3277=CARTESIAN_POINT ( 'NONE',  ( 1.010074371201537424, -0.4416272204090869735, -1.570717485485533249 ) ) ;
#3285=SHAPE_DEFINITION_REPRESENTATION ( #4778, #2104 ) ;
#3292=VERTEX_POINT ( 'NONE', #666 ) ;
#3301=CARTESIAN_POINT ( 'NONE',  ( 0.4330708661417322913, -0.9666437042230126009, -1.454455828411335583 ) ) ;
#3302=ORIENTED_EDGE ( 'NONE', *, *, #5061, .F. ) ;
#3311=B_SPLINE_CURVE_WITH_KNOTS ( 'NONE', 3,
 ( #6838, #3894, #6187, #1546, #6225, #3431, #5045, #3314, #5663, #3353 ),
 .UNSPECIFIED., .F., .F.,
 ( 4, 2, 2, 2, 4 ),
 ( 0.000000000000000000, 0.0005494620090385933520, 0.001098924018077186704, 0.001648386027115780056, 0.002197848036154373408 ),
 .UNSPECIFIED. ) ;
#3314=CARTESIAN_POINT ( 'NONE',  ( 0.4619485889667626077, 0.9755734897585890408, -1.553989674004692567 ) ) ;
#3315=EDGE_CURVE ( 'NONE', #443, #4433, #4268, .T. ) ;
#3317=DIRECTION ( 'NONE',  ( -7.708596820178695308E-30, 2.207829878515936732E-15, -1.000000000000000000 ) ) ;
#3325=CYLINDRICAL_SURFACE ( 'NONE', #1747, 0.2362204724409449341 ) ;
#3330=CARTESIAN_POINT ( 'NONE',  ( -0.9609181420092316461, -0.5141614760841496379, -1.361499588670821659 ) ) ;
#3334=EDGE_LOOP ( 'NONE', ( #4670, #6789, #195, #6417 ) ) ;
#3335=EDGE_LOOP ( 'NONE', ( #5494, #2642, #4330, #6989, #987, #654 ) ) ;
#3337=DIRECTION ( 'NONE',  ( -3.491481338843133750E-15, 1.000000000000000000, 0.000000000000000000 ) ) ;
#3338=CARTESIAN_POINT ( 'NONE',  ( 0.9883301303667288984, 0.4377665650305739842, -1.443420399700356072 ) ) ;
#3348=CARTESIAN_POINT ( 'NONE',  ( 0.2362204724409449341, 0.000000000000000000, -0.7983802283864780414 ) ) ;
#3349=CARTESIAN_POINT ( 'NONE',  ( -1.781909941321919274E-15, 0.000000000000000000, -1.397637795275591843 ) ) ;
#3353=CARTESIAN_POINT ( 'NONE',  ( 0.4700904924197906176, 0.9659644734970541657, -1.546597720061111847 ) ) ;
#3366=VERTEX_POINT ( 'NONE', #3348 ) ;
#3371=VERTEX_POINT ( 'NONE', #5579 ) ;
#3372=ORIENTED_EDGE ( 'NONE', *, *, #4289, .F. ) ;
#3374=DIRECTION ( 'NONE',  ( 1.000000000000000000, 0.000000000000000000, 2.207829878515936732E-15 ) ) ;
#3388=B_SPLINE_CURVE_WITH_KNOTS ( 'NONE', 3,
 ( #6912, #5671, #567, #2785, #7443, #1672, #2178, #4009, #6340, #3903, #1633, #5304, #6491, #4081, #1275, #3664, #641, #149 ),
 .UNSPECIFIED., .F., .F.,
 ( 4, 2, 2, 2, 2, 2, 2, 2, 4 ),
 ( 0.000000000000000000, 0.0002385177155853798715, 0.0004770354311707597429, 0.0009540708623415078849, 0.001431106293512256081, 0.001908141724683004277, 0.002385177155853752690, 0.002862212587024500886, 0.003816283449366009422 ),
 .UNSPECIFIED. ) ;
#3392=CARTESIAN_POINT ( 'NONE',  ( 0.9666437042230099363, 0.4330708661417423944, -1.454455828411337359 ) ) ;
#3393=DIRECTION ( 'NONE',  ( -1.047444401652940007E-14, 1.000000000000000000, -4.625929269271482167E-15 ) ) ;
#3397=DIRECTION ( 'NONE',  ( 0.000000000000000000, 0.000000000000000000, -1.000000000000000000 ) ) ;
#3405=VERTEX_POINT ( 'NONE', #3848 ) ;
#3409=EDGE_LOOP ( 'NONE', ( #4393, #1468, #3865, #6476 ) ) ;
#3415=ORIENTED_EDGE ( 'NONE', *, *, #1257, .F. ) ;
#3417=DIRECTION ( 'NONE',  ( -2.207829878515936732E-15, 0.000000000000000000, 1.000000000000000000 ) ) ;
#3421=ORIENTED_EDGE ( 'NONE', *, *, #6131, .F. ) ;
#3431=CARTESIAN_POINT ( 'NONE',  ( 0.4509662133831519593, 0.9917530546321599028, -1.563429817131423594 ) ) ;
#3433=DIRECTION ( 'NONE',  ( 0.000000000000000000, 0.000000000000000000, -1.000000000000000000 ) ) ;
#3440=CARTESIAN_POINT ( 'NONE',  ( -0.4406689276647596798, -0.9921522615226835429, -1.439080857166195271 ) ) ;
#3444=TOROIDAL_SURFACE ( 'NONE', #3830, 1.223643328182681289, 0.05905511811023622659 ) ;
#3449=CIRCLE ( 'NONE', #4058, 1.278433327952054555 ) ;
#3451=FACE_OUTER_BOUND ( 'NONE', #3334, .T. ) ;
#3452=DIRECTION ( 'NONE',  ( -1.000000000000000000, 0.000000000000000000, 0.000000000000000000 ) ) ;
#3464=ADVANCED_FACE ( 'NONE', ( #6948 ), #4145, .T. ) ;
#3467=EDGE_CURVE ( 'NONE', #811, #6826, #7318, .T. ) ;
#3472=AXIS2_PLACEMENT_3D ( 'NONE', #6986, #4195, #6449 ) ;
#3473=CARTESIAN_POINT ( 'NONE',  ( -0.9479499796399322165, 0.4353079511162203374, -1.456692913385826849 ) ) ;
#3477=VERTEX_POINT ( 'NONE', #2469 ) ;
#3478=CARTESIAN_POINT ( 'NONE',  ( -1.782879132931211256E-29, 1.702122929023921696E-15, -1.433776001880364026 ) ) ;
#3479=DIRECTION ( 'NONE',  ( 0.000000000000000000, 0.000000000000000000, -1.000000000000000000 ) ) ;
#3484=ORIENTED_EDGE ( 'NONE', *, *, #2021, .T. ) ;
#3496=DIRECTION ( 'NONE',  ( 2.207829878515936732E-15, -0.000000000000000000, -1.000000000000000000 ) ) ;
#3503=EDGE_CURVE ( 'NONE', #781, #1792, #1699, .T. ) ;
#3505=CARTESIAN_POINT ( 'NONE',  ( -0.4332839571663337774, 0.9726684123052331543, -1.452651065350217596 ) ) ;
#3508=CARTESIAN_POINT ( 'NONE',  ( -0.4720886891211135139, -0.9960023578760586194, -1.401719942879701586 ) ) ;
#3511=CARTESIAN_POINT ( 'NONE',  ( -0.4996352642496091345, -1.070877820178677498, -1.498503547059352403 ) ) ;
#3514=CIRCLE ( 'NONE', #6939, 1.278433327952054555 ) ;
#3518=ORIENTED_EDGE ( 'NONE', *, *, #4538, .F. ) ;
#3520=DIRECTION ( 'NONE',  ( 1.000000000000000000, 0.000000000000000000, -0.000000000000000000 ) ) ;
#3521=PLANE ( 'NONE',  #6590 ) ;
#3522=VERTEX_POINT ( 'NONE', #5503 ) ;
#3524=TOROIDAL_SURFACE ( 'NONE', #4018, 1.223643328182681289, 0.05905511811023622659 ) ;
#3529=ORIENTED_EDGE ( 'NONE', *, *, #5272, .F. ) ;
#3530=CARTESIAN_POINT ( 'NONE',  ( -0.4353079511162236681, -0.9479499796399322165, -1.456692913385828625 ) ) ;
#3534=DIRECTION ( 'NONE',  ( 7.708596820178695308E-30, -2.207829878515936732E-15, 1.000000000000000000 ) ) ;
#3535=CARTESIAN_POINT ( 'NONE',  ( 0.9411659768779468971, -0.4368170415251632077, -1.456692913385826849 ) ) ;
#3543=CARTESIAN_POINT ( 'NONE',  ( 0.4353079511162236126, -0.9479499796399308842, -1.456692913385826849 ) ) ;
#3545=CIRCLE ( 'NONE', #2094, 1.089828288828796676 ) ;
#3547=CARTESIAN_POINT ( 'NONE',  ( 0.000000000000000000, 0.000000000000000000, -1.574803149606299302 ) ) ;
#3548=DIRECTION ( 'NONE',  ( 0.000000000000000000, 8.881784197001249365E-16, 1.000000000000000000 ) ) ;
#3551=CARTESIAN_POINT ( 'NONE',  ( 6.500080172145040803E-30, -1.861696953619914682E-15, -1.361499588670820771 ) ) ;
#3558=ORIENTED_EDGE ( 'NONE', *, *, #5479, .F. ) ;
#3562=CARTESIAN_POINT ( 'NONE',  ( -0.5141614760841463072, -0.9609181420092334225, -1.361499588670821659 ) ) ;
#3565=CIRCLE ( 'NONE', #4177, 1.124634398195722973 ) ;
#3570=CARTESIAN_POINT ( 'NONE',  ( -1.085749034322388118, -0.4630669964643945868, -1.535808346805854319 ) ) ;
#3572=CIRCLE ( 'NONE', #7358, 0.9964144355006141485 ) ;
#3578=CARTESIAN_POINT ( 'NONE',  ( 1.048552902599916292, 0.4330708661417427274, -1.573978973432617279 ) ) ;
#3580=CARTESIAN_POINT ( 'NONE',  ( 0.000000000000000000, 0.000000000000000000, -1.546597720061111847 ) ) ;
#3583=UNCERTAINTY_MEASURE_WITH_UNIT (LENGTH_MEASURE( 1.000000000000000082E-05 ), #4188, 'distance_accuracy_value', 'NONE');
#3585=CARTESIAN_POINT ( 'NONE',  ( -0.4342019027940197673, 0.9783381746514265842, -1.450123259817210242 ) ) ;
#3586=DIRECTION ( 'NONE',  ( 1.000000000000000000, 0.000000000000000000, 4.625929269271482167E-15 ) ) ;
#3591=CARTESIAN_POINT ( 'NONE',  ( -0.4470329974975763010, -1.081428632361002951, -1.553789141944099894 ) ) ;
#3593=FACE_OUTER_BOUND ( 'NONE', #1617, .T. ) ;
#3594=ORIENTED_EDGE ( 'NONE', *, *, #5809, .T. ) ;
#3595=ORIENTED_EDGE ( 'NONE', *, *, #3315, .T. ) ;
#3602=ORIENTED_EDGE ( 'NONE', *, *, #6965, .T. ) ;
#3604=CARTESIAN_POINT ( 'NONE',  ( 0.9659644734970590507, -0.4700904924197804591, -1.546597720061111847 ) ) ;
#3608=CARTESIAN_POINT ( 'NONE',  ( -1.083410641227604554, -0.4508656291625843804, -1.549345754620972349 ) ) ;
#3616=DIRECTION ( 'NONE',  ( 1.000000000000000000, 0.000000000000000000, 2.207829878515936732E-15 ) ) ;
#3617=CARTESIAN_POINT ( 'NONE',  ( -1.075169953371344356, 0.4403524516313951920, -1.561970681382796045 ) ) ;
#3620=CARTESIAN_POINT ( 'NONE',  ( -0.4368378848980523088, -1.023372273685340117, -1.573834172653142183 ) ) ;
#3621=CARTESIAN_POINT ( 'NONE',  ( 0.4437903857718327738, -0.9221073153504517617, -1.453484209829403850 ) ) ;
#3622=DIRECTION ( 'NONE',  ( 1.000000000000000000, 0.000000000000000000, 0.000000000000000000 ) ) ;
#3625=CARTESIAN_POINT ( 'NONE',  ( 1.003669596044588941, -0.4445636273010707407, -1.568530023225017223 ) ) ;
#3626=DIRECTION ( 'NONE',  ( 0.000000000000000000, 0.000000000000000000, -1.000000000000000000 ) ) ;
#3629=CARTESIAN_POINT ( 'NONE',  ( 0.4330708661417322913, -0.9666437042230126009, -1.454455828411335583 ) ) ;
#3630=DIRECTION ( 'NONE',  ( -1.000000000000000000, 0.000000000000000000, 0.000000000000000000 ) ) ;
#3639=DIRECTION ( 'NONE',  ( 0.000000000000000000, 0.000000000000000000, -1.000000000000000000 ) ) ;
#3650=VERTEX_POINT ( 'NONE', #2054 ) ;
#3664=CARTESIAN_POINT ( 'NONE',  ( 0.4999740374263536569, -0.9773781006402563198, -1.373989084483999257 ) ) ;
#3665=DIRECTION ( 'NONE',  ( -2.207829878515936732E-15, 0.000000000000000000, 1.000000000000000000 ) ) ;
#3666=CARTESIAN_POINT ( 'NONE',  ( 0.8785537298370166281, -0.4700904924197814028, -1.433776001880362250 ) ) ;
#3672=DIRECTION ( 'NONE',  ( -1.047444401652940007E-14, 1.000000000000000000, -4.625929269271482167E-15 ) ) ;
#3674=EDGE_LOOP ( 'NONE', ( #2709, #6901, #1010, #546 ) ) ;
#3677=AXIS2_PLACEMENT_3D ( 'NONE', #2577, #3032, #743 ) ;
#3681=CARTESIAN_POINT ( 'NONE',  ( 0.4349192958999753555, 0.9810556462971140590, -1.448591228719267487 ) ) ;
#3682=AXIS2_PLACEMENT_3D ( 'NONE', #1093, #2219, #2282 ) ;
#3685=VERTEX_POINT ( 'NONE', #6073 ) ;
#3700=CIRCLE ( 'NONE', #7468, 1.168853328413307358 ) ;
#3701=CARTESIAN_POINT ( 'NONE',  ( 0.4330708661417322913, -1.048552902599920289, -1.573978973432616835 ) ) ;
#3727=( LENGTH_UNIT ( ) NAMED_UNIT ( * ) SI_UNIT ( $, .METRE. ) );
#3741=CARTESIAN_POINT ( 'NONE',  ( 0.4526810454163319730, 0.9044351468059360633, -1.447629383090422772 ) ) ;
#3744=DIRECTION ( 'NONE',  ( 0.000000000000000000, 0.000000000000000000, -1.000000000000000000 ) ) ;
#3749=CARTESIAN_POINT ( 'NONE',  ( -0.4508657589754699324, 1.083410700381146174, -1.549345605342071774 ) ) ;
#3754=EDGE_CURVE ( 'NONE', #4474, #2045, #1954, .T. ) ;
#3756=VERTEX_POINT ( 'NONE', #6399 ) ;
#3764=CARTESIAN_POINT ( 'NONE',  ( 0.9971724964170014527, -0.4476001829032997259, -1.429776958199368453 ) ) ;
#3765=VERTEX_POINT ( 'NONE', #5700 ) ;
#3766=CIRCLE ( 'NONE', #98, 1.278433327952055887 ) ;
#3781=CARTESIAN_POINT ( 'NONE',  ( 0.9659644734970493918, 0.4700904924198003876, -1.546597720061112069 ) ) ;
#3782=ORIENTED_EDGE ( 'NONE', *, *, #7229, .F. ) ;
#3783=DIRECTION ( 'NONE',  ( 1.000000000000000000, 0.000000000000000000, 4.625929269271482167E-15 ) ) ;
#3787=DIRECTION ( 'NONE',  ( -0.000000000000000000, -1.000000000000000000, 0.000000000000000000 ) ) ;
#3789=TOROIDAL_SURFACE ( 'NONE', #5752, 1.223643328182682621, 0.05905511811023622659 ) ;
#3793=EDGE_CURVE ( 'NONE', #6892, #4433, #4369, .T. ) ;
#3795=EDGE_LOOP ( 'NONE', ( #848, #2182, #5241, #7366 ) ) ;
#3800=EDGE_LOOP ( 'NONE', ( #6478, #3415, #6168, #114, #6291 ) ) ;
#3812=CIRCLE ( 'NONE', #4905, 0.2831409772408586822 ) ;
#3818=CARTESIAN_POINT ( 'NONE',  ( 0.8833138556571487054, -0.4663806185498647894, -1.436938405272744079 ) ) ;
#3820=FACE_OUTER_BOUND ( 'NONE', #2398, .T. ) ;
#3822=CARTESIAN_POINT ( 'NONE',  ( -0.4349482935633079972, 1.030265555772311048, -1.574803149606299302 ) ) ;
#3825=CIRCLE ( 'NONE', #415, 1.174991162294038771 ) ;
#3826=ORIENTED_EDGE ( 'NONE', *, *, #2711, .F. ) ;
#3830=AXIS2_PLACEMENT_3D ( 'NONE', #5624, #2169, #5702 ) ;
#3832=CARTESIAN_POINT ( 'NONE',  ( 0.4403525121893732686, 1.075170037517933164, -1.561970602951607168 ) ) ;
#3834=DIRECTION ( 'NONE',  ( 0.000000000000000000, 0.000000000000000000, 1.000000000000000000 ) ) ;
#3835=ORIENTED_EDGE ( 'NONE', *, *, #2530, .T. ) ;
#3840=ADVANCED_FACE ( 'NONE', ( #4501 ), #4030, .T. ) ;
#3842=CARTESIAN_POINT ( 'NONE',  ( 0.9983959133492292803, -0.4514965799695651039, -1.424958590981960205 ) ) ;
#3846=ORIENTED_EDGE ( 'NONE', *, *, #4497, .F. ) ;
#3848=CARTESIAN_POINT ( 'NONE',  ( 0.9609181420092280934, 0.5141614760841562992, -1.361499588670821659 ) ) ;
#3851=CARTESIAN_POINT ( 'NONE',  ( 0.4330708661417322913, 1.048552902599920289, -1.573978973432616835 ) ) ;
#3858=CARTESIAN_POINT ( 'NONE',  ( 1.003668447264486563, 0.4445641707283079502, -1.568529612473645418 ) ) ;
#3864=CARTESIAN_POINT ( 'NONE',  ( -0.9971723906835420204, -0.4475999628372231975, -1.429777239771659270 ) ) ;
#3865=ORIENTED_EDGE ( 'NONE', *, *, #4450, .F. ) ;
#3869=ORIENTED_EDGE ( 'NONE', *, *, #5844, .F. ) ;
#3870=ORIENTED_EDGE ( 'NONE', *, *, #1246, .F. ) ;
#3873=CARTESIAN_POINT ( 'NONE',  ( 0.4330708661417322913, 0.9666437042230126009, -1.454455828411335583 ) ) ;
#3874=ORIENTED_EDGE ( 'NONE', *, *, #6131, .T. ) ;
#3876=ORIENTED_EDGE ( 'NONE', *, *, #4496, .F. ) ;
#3891=AXIS2_PLACEMENT_3D ( 'NONE', #1602, #6276, #2789 ) ;
#3894=CARTESIAN_POINT ( 'NONE',  ( 0.4349482935633082747, 1.030265555772310826, -1.574803149606299302 ) ) ;
#3903=CARTESIAN_POINT ( 'NONE',  ( 0.4596433552321258498, -0.9990286922241453649, -1.415369843883346412 ) ) ;
#3906=CARTESIAN_POINT ( 'NONE',  ( -0.9983958463931797978, -0.4514963146295112306, -1.424958914991361736 ) ) ;
#3909=AXIS2_PLACEMENT_3D ( 'NONE', #4690, #7060, #2921 ) ;
#3912=ORIENTED_EDGE ( 'NONE', *, *, #4674, .F. ) ;
#3916=CARTESIAN_POINT ( 'NONE',  ( 0.9983959133492219529, 0.4514965799695863091, -1.424958590981962425 ) ) ;
#3926=AXIS2_PLACEMENT_3D ( 'NONE', #5515, #313, #6086 ) ;
#3930=ADVANCED_FACE ( 'NONE', ( #5988 ), #3789, .T. ) ;
#3935=EDGE_CURVE ( 'NONE', #1079, #1691, #1720, .T. ) ;
#3937=CARTESIAN_POINT ( 'NONE',  ( -0.4627504720074766542, -0.8884022185686314410, -1.439912370850675138 ) ) ;
#3942=EDGE_LOOP ( 'NONE', ( #1080, #3259, #5068, #6627, #1656, #6013, #7493, #6481, #6381, #971, #7145, #2118 ) ) ;
#3943=AXIS2_PLACEMENT_3D ( 'NONE', #6964, #4061, #1046 ) ;
#3944=CARTESIAN_POINT ( 'NONE',  ( -0.8989373009621118849, 0.4559215864680308816, -1.445239633971734383 ) ) ;
#3946=DIRECTION ( 'NONE',  ( 0.000000000000000000, -4.440892098500625373E-15, 1.000000000000000000 ) ) ;
#3953=ORIENTED_EDGE ( 'NONE', *, *, #2021, .F. ) ;
#3967=CARTESIAN_POINT ( 'NONE',  ( 0.8989373009621074440, 0.4559215864680435937, -1.445239633971736604 ) ) ;
#3980=DIRECTION ( 'NONE',  ( 7.708596820178695308E-30, -2.207829878515936732E-15, 1.000000000000000000 ) ) ;
#3985=CARTESIAN_POINT ( 'NONE',  ( -0.4330708661417321803, -0.9697097640641213490, -1.453662949853145481 ) ) ;
#3986=ORIENTED_EDGE ( 'NONE', *, *, #6306, .T. ) ;
#4002=CARTESIAN_POINT ( 'NONE',  ( 0.9479499796399277756, 0.4353079511162336046, -1.456692913385828625 ) ) ;
#4003=CARTESIAN_POINT ( 'NONE',  ( 0.4921259842519683514, 0.000000000000000000, -2.204724409448820754 ) ) ;
#4007=AXIS2_PLACEMENT_3D ( 'NONE', #1362, #6575, #4238 ) ;
#4009=CARTESIAN_POINT ( 'NONE',  ( 0.4475999628372195893, -0.9971723906835419093, -1.429777239771657271 ) ) ;
#4011=CIRCLE ( 'NONE', #7303, 1.278433327952056553 ) ;
#4013=CARTESIAN_POINT ( 'NONE',  ( -0.4349192646538860285, -0.9810555383103382043, -1.448591292758283133 ) ) ;
#4018=AXIS2_PLACEMENT_3D ( 'NONE', #6576, #1467, #6191 ) ;
#4020=VERTEX_POINT ( 'NONE', #324 ) ;
#4030=TOROIDAL_SURFACE ( 'NONE', #730, 1.043121362164705745, 0.05905511811023622659 ) ;
#4033=MANIFOLD_SOLID_BREP ( 'Fillet2', #2613 ) ;
#4037=CARTESIAN_POINT ( 'NONE',  ( -1.010074371201531429, -0.4416272204091005738, -1.570717485485532583 ) ) ;
#4042=AXIS2_PLACEMENT_3D ( 'NONE', #4263, #2462, #1894 ) ;
#4044=CARTESIAN_POINT ( 'NONE',  ( -0.9221077491748242982, 0.4437902010346525539, -1.453484313640521552 ) ) ;
#4048=CARTESIAN_POINT ( 'NONE',  ( -0.5141614760841463072, -0.9609181420092334225, -1.361499588670821659 ) ) ;
#4053=CARTESIAN_POINT ( 'NONE',  ( 0.000000000000000000, 0.000000000000000000, -1.515748031496062964 ) ) ;
#4054=VERTEX_POINT ( 'NONE', #2232 ) ;
#4058=AXIS2_PLACEMENT_3D ( 'NONE', #365, #2686, #4952 ) ;
#4061=DIRECTION ( 'NONE',  ( -1.000000000000000000, -0.000000000000000000, -4.625929269271482167E-15 ) ) ;
#4072=CARTESIAN_POINT ( 'NONE',  ( -1.702122929023921696E-15, 0.000000000000000000, -1.433776001880364026 ) ) ;
#4073=EDGE_CURVE ( 'NONE', #2290, #5576, #953, .T. ) ;
#4081=CARTESIAN_POINT ( 'NONE',  ( 0.4843356560173194270, -0.9895441027518980803, -1.389133886014302099 ) ) ;
#4085=CARTESIAN_POINT ( 'NONE',  ( -0.4878045971889968246, -1.078368813366570755, -1.510181706589752260 ) ) ;
#4093=CARTESIAN_POINT ( 'NONE',  ( -0.4700904924197903401, -0.9659644734970543878, -1.546597720061111847 ) ) ;
#4099=DIRECTION ( 'NONE',  ( -4.625929269271482167E-15, 0.000000000000000000, 1.000000000000000000 ) ) ;
#4102=CARTESIAN_POINT ( 'NONE',  ( 1.085572762089316079, -0.4589126309195263320, -1.540322683979783003 ) ) ;
#4103=EDGE_LOOP ( 'NONE', ( #5994, #7033, #3168, #6204 ) ) ;
#4113=AXIS2_PLACEMENT_3D ( 'NONE', #4362, #5560, #318 ) ;
#4115=CARTESIAN_POINT ( 'NONE',  ( 0.4466264210910796950, -0.9159926810392086116, -1.451746030331783510 ) ) ;
#4121=CARTESIAN_POINT ( 'NONE',  ( -0.4330708661417317362, -1.048552902599920955, -1.573978973432617279 ) ) ;
#4129=AXIS2_PLACEMENT_3D ( 'NONE', #564, #3393, #1667 ) ;
#4135=CIRCLE ( 'NONE', #6458, 1.377952755905511806 ) ;
#4140=CARTESIAN_POINT ( 'NONE',  ( -1.060348472569314193, -0.4341579012690721662, -1.570964862939435269 ) ) ;
#4145=TOROIDAL_SURFACE ( 'NONE', #1584, 1.043121362164705745, 0.05905511811023622659 ) ;
#4146=EDGE_CURVE ( 'NONE', #2327, #7237, #4366, .T. ) ;
#4148=CARTESIAN_POINT ( 'NONE',  ( -1.048552902599921843, 0.4330708661417285721, -1.573978973432616835 ) ) ;
#4149=FACE_OUTER_BOUND ( 'NONE', #434, .T. ) ;
#4156=CARTESIAN_POINT ( 'NONE',  ( 1.078368654584398456, 0.4878048847236929331, -1.510181419419387439 ) ) ;
#4167=AXIS2_PLACEMENT_3D ( 'NONE', #59, #6484, #1230 ) ;
#4171=AXIS2_PLACEMENT_3D ( 'NONE', #908, #3236, #337 ) ;
#4174=CARTESIAN_POINT ( 'NONE',  ( 0.4843361811957743734, 0.9895437626941967491, -1.389133361342958173 ) ) ;
#4177=AXIS2_PLACEMENT_3D ( 'NONE', #5920, #6445, #1193 ) ;
#4185=CIRCLE ( 'NONE', #6031, 1.168853328413307135 ) ;
#4188=( CONVERSION_BASED_UNIT ( 'INCH', #1507 ) LENGTH_UNIT ( ) NAMED_UNIT ( #6920 ) );
#4191=CARTESIAN_POINT ( 'NONE',  ( 1.044891351410285552, 0.4330708661417424499, -1.574550377471545470 ) ) ;
#4195=DIRECTION ( 'NONE',  ( 0.000000000000000000, 0.000000000000000000, -1.000000000000000000 ) ) ;
#4196=CARTESIAN_POINT ( 'NONE',  ( 0.9783381746514221433, 0.4342019027940302034, -1.450123259817210908 ) ) ;
#4201=CARTESIAN_POINT ( 'NONE',  ( 0.000000000000000000, 0.000000000000000000, -1.484898342931014303 ) ) ;
#4214=CARTESIAN_POINT ( 'NONE',  ( 0.4330708661417321803, 0.9697097892794909191, -1.453662943332485247 ) ) ;
#4218=ORIENTED_EDGE ( 'NONE', *, *, #2847, .F. ) ;
#4222=PRODUCT_CONTEXT ( 'NONE', #6055, 'mechanical' ) ;
#4223=DIRECTION ( 'NONE',  ( 1.000000000000000000, 0.000000000000000000, -0.000000000000000000 ) ) ;
#4232=CARTESIAN_POINT ( 'NONE',  ( 0.5072022184710041071, -1.064268091466991084, -1.491294347567119427 ) ) ;
#4236=CARTESIAN_POINT ( 'NONE',  ( 1.080458355692609729, 0.4837911690062530745, -1.514208178040841846 ) ) ;
#4238=DIRECTION ( 'NONE',  ( 1.000000000000000000, 0.000000000000000000, 2.095133389269358970E-15 ) ) ;
#4239=CARTESIAN_POINT ( 'NONE',  ( -0.4338950423154138147, 1.037563309807725043, -1.574803149606299302 ) ) ;
#4241=ORIENTED_EDGE ( 'NONE', *, *, #6733, .F. ) ;
#4242=CARTESIAN_POINT ( 'NONE',  ( -0.9810555383103384264, 0.4349192646538826978, -1.448591292758282245 ) ) ;
#4247=CARTESIAN_POINT ( 'NONE',  ( 0.4332776171645018048, 1.054581729003112311, -1.572814845875644352 ) ) ;
#4249=DIRECTION ( 'NONE',  ( 1.000000000000000000, 0.000000000000000000, -0.000000000000000000 ) ) ;
#4255=CIRCLE ( 'NONE', #6333, 1.168853328413307135 ) ;
#4261=CARTESIAN_POINT ( 'NONE',  ( 1.083679028610385009, -0.4756000659977862588, -1.522578585053779188 ) ) ;
#4263=CARTESIAN_POINT ( 'NONE',  ( 1.718248690375545225E-15, -0.4921259842519648542, -2.204724409448822975 ) ) ;
#4266=CARTESIAN_POINT ( 'NONE',  ( -0.4700904924197908397, 0.8785537298370134085, -1.433776001880364470 ) ) ;
#4268=CIRCLE ( 'NONE', #6226, 1.168853328413308690 ) ;
#4270=DIRECTION ( 'NONE',  ( 0.000000000000000000, 0.000000000000000000, -1.000000000000000000 ) ) ;
#4272=CARTESIAN_POINT ( 'NONE',  ( 1.054581729003108759, 0.4332776171645121299, -1.572814845875644352 ) ) ;
#4278=CARTESIAN_POINT ( 'NONE',  ( -0.9773781006402579852, 0.4999740374263504372, -1.373989084483999257 ) ) ;
#4280=CARTESIAN_POINT ( 'NONE',  ( 0.2952755905511811885, 3.616083068348484413E-17, -0.7983802283864783744 ) ) ;
#4284=ORIENTED_EDGE ( 'NONE', *, *, #2388, .F. ) ;
#4289=EDGE_CURVE ( 'NONE', #1079, #7462, #4499, .T. ) ;
#4291=DIRECTION ( 'NONE',  ( -1.000000000000000000, 0.000000000000000000, 0.000000000000000000 ) ) ;
#4303=EDGE_CURVE ( 'NONE', #3366, #1484, #4699, .T. ) ;
#4314=DIRECTION ( 'NONE',  ( -1.000000000000000000, 0.000000000000000000, 0.000000000000000000 ) ) ;
#4316=DIRECTION ( 'NONE',  ( 0.000000000000000000, 0.000000000000000000, -1.000000000000000000 ) ) ;
#4320=CARTESIAN_POINT ( 'NONE',  ( 0.000000000000000000, 0.000000000000000000, -2.204724409448820754 ) ) ;
#4323=CARTESIAN_POINT ( 'NONE',  ( -0.9783380834473015542, 0.4342018836190565390, -1.450123305573143284 ) ) ;
#4324=CARTESIAN_POINT ( 'NONE',  ( -0.4630671888207402165, 1.085749034841582139, -1.535808138920397026 ) ) ;
#4326=ORIENTED_EDGE ( 'NONE', *, *, #7279, .T. ) ;
#4327=FACE_OUTER_BOUND ( 'NONE', #3942, .T. ) ;
#4329=CARTESIAN_POINT ( 'NONE',  ( 0.4330708661417322913, 0.9666437042230126009, -1.454455828411335583 ) ) ;
#4330=ORIENTED_EDGE ( 'NONE', *, *, #5850, .F. ) ;
#4337=CARTESIAN_POINT ( 'NONE',  ( -1.037563309807726375, 0.4338950423154108171, -1.574803149606299302 ) ) ;
#4341=VERTEX_POINT ( 'NONE', #6697 ) ;
#4347=EDGE_CURVE ( 'NONE', #2144, #6423, #1167, .T. ) ;
#4348=CARTESIAN_POINT ( 'NONE',  ( 0.4341579012690690575, -1.060348472569314415, -1.570964862939435491 ) ) ;
#4356=DIRECTION ( 'NONE',  ( -1.000000000000000000, -1.047067131017168686E-14, 0.000000000000000000 ) ) ;
#4357=CARTESIAN_POINT ( 'NONE',  ( -0.4348450248026697884, 1.063161309294320178, -1.569784497862150463 ) ) ;
#4362=CARTESIAN_POINT ( 'NONE',  ( 1.795185198899822598E-15, -0.5141614760841421994, -2.204724409448823419 ) ) ;
#4363=ORIENTED_EDGE ( 'NONE', *, *, #7014, .T. ) ;
#4364=CARTESIAN_POINT ( 'NONE',  ( 0.4368378848980529749, -1.023372273685339895, -1.573834172653142627 ) ) ;
#4366=CIRCLE ( 'NONE', #583, 1.259842519685039131 ) ;
#4369=B_SPLINE_CURVE_WITH_KNOTS ( 'NONE', 3,
 ( #4002, #1582, #7395, #2306, #4607, #4640, #3967, #7430, #1050, #6258 ),
 .UNSPECIFIED., .F., .F.,
 ( 4, 2, 2, 2, 4 ),
 ( 0.000000000000000000, 0.0005216184974661230425, 0.001043236994932246085, 0.001564855492398369019, 0.002086473989864492170 ),
 .UNSPECIFIED. ) ;
#4372=CARTESIAN_POINT ( 'NONE',  ( 0.9960021845704909449, -0.4720891361949376419, -1.401719468380311140 ) ) ;
#4373=ORIENTED_EDGE ( 'NONE', *, *, #4764, .F. ) ;
#4376=ORIENTED_EDGE ( 'NONE', *, *, #2620, .F. ) ;
#4379=ORIENTED_EDGE ( 'NONE', *, *, #2246, .T. ) ;
#4380=TOROIDAL_SURFACE ( 'NONE', #1313, 1.223643328182682621, 0.05905511811023622659 ) ;
#4385=CARTESIAN_POINT ( 'NONE',  ( -0.9411659768779426782, -0.4368170415251763639, -1.456692913385828847 ) ) ;
#4390=CARTESIAN_POINT ( 'NONE',  ( 0.4627498550472184946, 0.8884031170519962606, -1.439912866901231547 ) ) ;
#4393=ORIENTED_EDGE ( 'NONE', *, *, #5374, .T. ) ;
#4394=CARTESIAN_POINT ( 'NONE',  ( -0.9867938558989117759, 0.4882975260543697682, -1.385219839936550956 ) ) ;
#4397=DIRECTION ( 'NONE',  ( -1.000000000000000000, 0.000000000000000000, 0.000000000000000000 ) ) ;
#4424=CIRCLE ( 'NONE', #6626, 0.9964144355006141485 ) ;
#4426=FACE_OUTER_BOUND ( 'NONE', #1566, .T. ) ;
#4428=AXIS2_PLACEMENT_3D ( 'NONE', #7416, #3337, #966 ) ;
#4429=TOROIDAL_SURFACE ( 'NONE', #1983, 1.223643328182682621, 0.05905511811023622659 ) ;
#4430=DIRECTION ( 'NONE',  ( 0.000000000000000000, 1.000000000000000000, 2.193342766891360832E-15 ) ) ;
#4432=CARTESIAN_POINT ( 'NONE',  ( -0.4659838021914858852, 0.9705345056685065197, -1.550372027848314405 ) ) ;
#4433=VERTEX_POINT ( 'NONE', #4976 ) ;
#4435=EDGE_CURVE ( 'NONE', #3477, #1882, #6649, .T. ) ;
#4447=EDGE_CURVE ( 'NONE', #5491, #6357, #457, .T. ) ;
#4450=EDGE_CURVE ( 'NONE', #5491, #5648, #3514, .T. ) ;
#4455=( CONVERSION_BASED_UNIT ( 'INCH', #2121 ) LENGTH_UNIT ( ) NAMED_UNIT ( #6292 ) );
#4458=ORIENTED_EDGE ( 'NONE', *, *, #7285, .F. ) ;
#4463=VERTEX_POINT ( 'NONE', #996 ) ;
#4464=EDGE_LOOP ( 'NONE', ( #3106, #6620, #4993, #3953, #2784, #6167 ) ) ;
#4469=DIRECTION ( 'NONE',  ( -1.000000000000000000, 0.000000000000000000, 0.000000000000000000 ) ) ;
#4472=CARTESIAN_POINT ( 'NONE',  ( -0.4416276115803083879, 1.010073413237866813, -1.570717210673253428 ) ) ;
#4474=VERTEX_POINT ( 'NONE', #5133 ) ;
#4477=CARTESIAN_POINT ( 'NONE',  ( -0.9990286922241452539, -0.4596433552321293470, -1.415369843883348411 ) ) ;
#4480=CARTESIAN_POINT ( 'NONE',  ( -0.9857970000181568437, -0.4541662050560865138, -1.560880783937514726 ) ) ;
#4488=VERTEX_POINT ( 'NONE', #6771 ) ;
#4490=ORIENTED_EDGE ( 'NONE', *, *, #7513, .T. ) ;
#4493=DIRECTION ( 'NONE',  ( -3.491481338843133750E-15, 1.000000000000000000, 0.000000000000000000 ) ) ;
#4496=EDGE_CURVE ( 'NONE', #4488, #2144, #1427, .T. ) ;
#4497=EDGE_CURVE ( 'NONE', #3371, #2290, #3766, .T. ) ;
#4499=CIRCLE ( 'NONE', #1171, 1.223643328182681289 ) ;
#4501=FACE_OUTER_BOUND ( 'NONE', #1485, .T. ) ;
#4503=CARTESIAN_POINT ( 'NONE',  ( 1.641312181851266274E-15, -0.4700904924197871204, -2.204724409448822975 ) ) ;
#4509=ORIENTED_EDGE ( 'NONE', *, *, #2620, .T. ) ;
#4516=DIRECTION ( 'NONE',  ( 4.647695938698652561E-15, 1.421085471520200372E-14, -1.000000000000000000 ) ) ;
#4520=ORIENTED_EDGE ( 'NONE', *, *, #5374, .F. ) ;
#4523=CARTESIAN_POINT ( 'NONE',  ( -0.4353079511162236681, 0.9479499796399324385, -1.456692913385828625 ) ) ;
#4529=ADVANCED_FACE ( 'NONE', ( #2221 ), #6818, .T. ) ;
#4538=EDGE_CURVE ( 'NONE', #7001, #3252, #3179, .T. ) ;
#4550=DIRECTION ( 'NONE',  ( -1.000000000000000000, 0.000000000000000000, 0.000000000000000000 ) ) ;
#4554=CARTESIAN_POINT ( 'NONE',  ( -0.9696655408443565216, -0.5073440712898458216, -1.367310953805257023 ) ) ;
#4556=AXIS2_PLACEMENT_3D ( 'NONE', #914, #6689, #7256 ) ;
#4557=CARTESIAN_POINT ( 'NONE',  ( 6.500080172145040803E-30, -1.861696953619914682E-15, -1.361499588670820771 ) ) ;
#4566=ORIENTED_EDGE ( 'NONE', *, *, #4674, .T. ) ;
#4568=B_SPLINE_CURVE_WITH_KNOTS ( 'NONE', 3,
 ( #5551, #2063, #6721, #3625, #3277, #422, #4583, #5589 ),
 .UNSPECIFIED., .F., .F.,
 ( 4, 2, 2, 4 ),
 ( -7.690028535486727074E-06, 0.001102852776893269420, 0.001658124179607644048, 0.002213395582322019110 ),
 .UNSPECIFIED. ) ;
#4583=CARTESIAN_POINT ( 'NONE',  ( 1.030265823844203288, -0.4349482548737160781, -1.574803149606299524 ) ) ;
#4585=FACE_OUTER_BOUND ( 'NONE', #4103, .T. ) ;
#4591=DIRECTION ( 'NONE',  ( -1.000000000000000000, -0.000000000000000000, -4.625929269271482167E-15 ) ) ;
#4593=CARTESIAN_POINT ( 'NONE',  ( 1.070856907295309801, -0.4375700573520588943, -1.565644078513316106 ) ) ;
#4597=ORIENTED_EDGE ( 'NONE', *, *, #5542, .T. ) ;
#4601=VERTEX_POINT ( 'NONE', #33 ) ;
#4602=DIRECTION ( 'NONE',  ( -1.000000000000000000, 0.000000000000000000, 0.000000000000000000 ) ) ;
#4603=CARTESIAN_POINT ( 'NONE',  ( -0.9659644734970558311, 0.4700904924197872314, -1.546597720061112069 ) ) ;
#4607=CARTESIAN_POINT ( 'NONE',  ( 0.9159932075028710541, 0.4466261709646471290, -1.451746187131335519 ) ) ;
#4609=CARTESIAN_POINT ( 'NONE',  ( -1.003669596044583168, -0.4445636273010842854, -1.568530023225017223 ) ) ;
#4610=AXIS2_PLACEMENT_3D ( 'NONE', #6285, #2727, #2833 ) ;
#4614=DIRECTION ( 'NONE',  ( -1.000000000000000000, 0.000000000000000000, 0.000000000000000000 ) ) ;
#4615=EDGE_CURVE ( 'NONE', #5146, #6892, #3272, .T. ) ;
#4616=CARTESIAN_POINT ( 'NONE',  ( -0.8785537298370134085, 0.4700904924197875645, -1.433776001880362250 ) ) ;
#4618=CIRCLE ( 'NONE', #6942, 1.278433327952054999 ) ;
#4640=CARTESIAN_POINT ( 'NONE',  ( 0.9044351468059328436, 0.4526810454163415209, -1.447629383090424993 ) ) ;
#4642=CARTESIAN_POINT ( 'NONE',  ( -1.056523642887401415, -0.5141614760841493048, -1.484898342931014303 ) ) ;
#4643=CARTESIAN_POINT ( 'NONE',  ( -0.4338950423154138147, 1.037563309807725043, -1.574803149606299302 ) ) ;
#4644=TOROIDAL_SURFACE ( 'NONE', #1967, 1.223643328182681289, 0.05905511811023622659 ) ;
#4653=CARTESIAN_POINT ( 'NONE',  ( -0.4514963146295076224, -0.9983958463931812410, -1.424958914991361292 ) ) ;
#4658=ORIENTED_EDGE ( 'NONE', *, *, #3271, .F. ) ;
#4664=EDGE_CURVE ( 'NONE', #6137, #4020, #5030, .T. ) ;
#4668=DIRECTION ( 'NONE',  ( 1.000000000000000000, 0.000000000000000000, -0.000000000000000000 ) ) ;
#4670=ORIENTED_EDGE ( 'NONE', *, *, #2568, .T. ) ;
#4674=EDGE_CURVE ( 'NONE', #3477, #4341, #2057, .T. ) ;
#4675=CARTESIAN_POINT ( 'NONE',  ( -0.4921259842519648542, 0.000000000000000000, -2.204724409448822975 ) ) ;
#4677=CARTESIAN_POINT ( 'NONE',  ( -0.4330708661417320138, -0.9604263920613191896, -1.456063616177416087 ) ) ;
#4678=CARTESIAN_POINT ( 'NONE',  ( -1.080458485393810397, -0.4837908950006702402, -1.514208454829283346 ) ) ;
#4685=DIRECTION ( 'NONE',  ( 1.000000000000000000, 0.000000000000000000, 0.000000000000000000 ) ) ;
#4689=CARTESIAN_POINT ( 'NONE',  ( 0.9666437042230172638, -0.4330708661417221883, -1.454455828411335583 ) ) ;
#4690=CARTESIAN_POINT ( 'NONE',  ( 1.512058847530478993E-15, -0.4330708661417287941, -2.204724409448822975 ) ) ;
#4693=EDGE_LOOP ( 'NONE', ( #6248, #895, #3011, #2086, #3594, #1181, #4597, #3874, #3595, #1026, #4509 ) ) ;
#4699=LINE ( 'NONE', #5403, #90 ) ;
#4702=CARTESIAN_POINT ( 'NONE',  ( -1.037563309807726375, 0.4338950423154108171, -1.574803149606299302 ) ) ;
#4714=CARTESIAN_POINT ( 'NONE',  ( -0.9659644734970528335, -0.4700904924197936707, -1.546597720061111847 ) ) ;
#4727=CARTESIAN_POINT ( 'NONE',  ( -0.4762527114670029316, 0.9941396836775485690, -1.397361282224858892 ) ) ;
#4741=DIRECTION ( 'NONE',  ( -1.000000000000000000, -3.516270216102430554E-15, 0.000000000000000000 ) ) ;
#4743=AXIS2_PLACEMENT_3D ( 'NONE', #911, #982, #3276 ) ;
#4744=CARTESIAN_POINT ( 'NONE',  ( 0.4514965799695757620, 0.9983959133492256166, -1.424958590981960871 ) ) ;
#4754=CARTESIAN_POINT ( 'NONE',  ( -1.070856827570678238, -0.4375700189966333364, -1.565644132322241644 ) ) ;
#4762=ADVANCED_FACE ( 'NONE', ( #5392 ), #710, .T. ) ;
#4764=EDGE_CURVE ( 'NONE', #1492, #3685, #5391, .T. ) ;
#4766=EDGE_CURVE ( 'NONE', #781, #3685, #4568, .T. ) ;
#4768=CARTESIAN_POINT ( 'NONE',  ( -0.4330708661417322913, 0.9666437042230143772, -1.454455828411337359 ) ) ;
#4769=DIRECTION ( 'NONE',  ( 0.000000000000000000, 0.000000000000000000, 1.000000000000000000 ) ) ;
#4770=CARTESIAN_POINT ( 'NONE',  ( 1.064252964791818634, 0.5072158114893481340, -1.491281854710859278 ) ) ;
#4774=FACE_OUTER_BOUND ( 'NONE', #4464, .T. ) ;
#4778=PRODUCT_DEFINITION_SHAPE ( 'NONE', 'NONE',  #5928 ) ;
#4782=CIRCLE ( 'NONE', #1464, 1.043121362164705745 ) ;
#4785=AXIS2_PLACEMENT_3D ( 'NONE', #4503, #6835, #416 ) ;
#4793=TOROIDAL_SURFACE ( 'NONE', #281, 1.124634398195722973, 0.05905511811023622659 ) ;
#4798=CARTESIAN_POINT ( 'NONE',  ( -1.078368813366568979, -0.4878045971890005994, -1.510181706589752038 ) ) ;
#4802=ORIENTED_EDGE ( 'NONE', *, *, #6913, .F. ) ;
#4812=CARTESIAN_POINT ( 'NONE',  ( -0.5141614760841463072, 0.9609181420092333115, -1.361499588670821659 ) ) ;
#4814=DIRECTION ( 'NONE',  ( -1.047444401652940007E-14, 1.000000000000000000, -4.625929269271482167E-15 ) ) ;
#4816=CARTESIAN_POINT ( 'NONE',  ( 0.4333661275892078946, -1.041228047528454548, -1.574803149606299302 ) ) ;
#4817=DIRECTION ( 'NONE',  ( -1.000000000000000000, 0.000000000000000000, 0.000000000000000000 ) ) ;
#4819=CARTESIAN_POINT ( 'NONE',  ( 0.000000000000000000, 0.000000000000000000, -1.484898342931014303 ) ) ;
#4825=CARTESIAN_POINT ( 'NONE',  ( 0.4348450248026701215, 1.063161309294319512, -1.569784497862150241 ) ) ;
#4828=ORIENTED_EDGE ( 'NONE', *, *, #4664, .F. ) ;
#4829=ORIENTED_EDGE ( 'NONE', *, *, #6781, .T. ) ;
#4833=VERTEX_POINT ( 'NONE', #3392 ) ;
#4837=PRODUCT ( 'MAT-019 Puller', 'MAT-019 Puller', '', ( #4222 ) ) ;
#4838=CARTESIAN_POINT ( 'NONE',  ( -0.4526810454163320840, 0.9044351468059372845, -1.447629383090424549 ) ) ;
#4839=CARTESIAN_POINT ( 'NONE',  ( -1.080458485393813062, 0.4837908950006628572, -1.514208454829284234 ) ) ;
#4841=CARTESIAN_POINT ( 'NONE',  ( 0.4332776154273901836, -1.054581703806071413, -1.572814851683855819 ) ) ;
#4844=CARTESIAN_POINT ( 'NONE',  ( 1.070856907295301363, 0.4375700573520810432, -1.565644078513316551 ) ) ;
#4848=FACE_OUTER_BOUND ( 'NONE', #6998, .T. ) ;
#4852=CARTESIAN_POINT ( 'NONE',  ( -0.4589126309195370457, 1.085572762089311416, -1.540322683979783003 ) ) ;
#4858=ORIENTED_EDGE ( 'NONE', *, *, #3503, .T. ) ;
#4859=CARTESIAN_POINT ( 'NONE',  ( 0.4445636273010810657, -1.003669596044584278, -1.568530023225017223 ) ) ;
#4862=B_SPLINE_CURVE_WITH_KNOTS ( 'NONE', 3,
 ( #4702, #2333, #8, #6359, #584, #5826, #7036, #7000, #2940, #4603 ),
 .UNSPECIFIED., .F., .F.,
 ( 4, 2, 2, 2, 4 ),
 ( 0.000000000000000000, 0.0005494620090385951951, 0.001098924018077190390, 0.001648386027115785694, 0.002197848036154380780 ),
 .UNSPECIFIED. ) ;
#4866=ORIENTED_EDGE ( 'NONE', *, *, #6914, .F. ) ;
#4874=CARTESIAN_POINT ( 'NONE',  ( 1.081428707249772803, -0.4470331066954845167, -1.553789012478535403 ) ) ;
#4875=ADVANCED_FACE ( 'NONE', ( #5084 ), #4429, .T. ) ;
#4884=FACE_OUTER_BOUND ( 'NONE', #3674, .T. ) ;
#4888=CARTESIAN_POINT ( 'NONE',  ( 0.4330708661417321248, -1.044891351410288216, -1.574550377471545692 ) ) ;
#4900=AXIS2_PLACEMENT_3D ( 'NONE', #6804, #5744, #6272 ) ;
#4901=ORIENTED_EDGE ( 'NONE', *, *, #3935, .T. ) ;
#4905=AXIS2_PLACEMENT_3D ( 'NONE', #2209, #5768, #7435 ) ;
#4907=EDGE_LOOP ( 'NONE', ( #1072, #774, #4376, #6460, #3484, #4858, #7009, #6202, #3125, #6567, #3986 ) ) ;
#4908=CARTESIAN_POINT ( 'NONE',  ( 0.9895437626942018561, -0.4843361811957641594, -1.389133361342958173 ) ) ;
#4928=B_SPLINE_CURVE_WITH_KNOTS ( 'NONE', 3,
 ( #2449, #6586, #81, #6999, #4174, #6515, #2407, #42, #6550, #4744, #1334, #7077, #1751, #3681, #1883, #1788, #4214, #5942 ),
 .UNSPECIFIED., .F., .F.,
 ( 4, 2, 2, 2, 2, 2, 2, 2, 4 ),
 ( -8.121667112567890505E-06, 0.0009422843086939710396, 0.001417487296597246807, 0.001892690284500522574, 0.002367893272403798557, 0.002843096260307074324, 0.003318299248210350525, 0.003555900742161984072, 0.003793502236113617618 ),
 .UNSPECIFIED. ) ;
#4930=DIRECTION ( 'NONE',  ( 3.491481338843133750E-15, -1.000000000000000000, -4.625929269271482167E-15 ) ) ;
#4932=CARTESIAN_POINT ( 'NONE',  ( -0.9883299873891312481, 0.4377664870282915177, -1.443420526770070600 ) ) ;
#4933=CARTESIAN_POINT ( 'NONE',  ( -0.4837911690062416947, 1.080458355692614836, -1.514208178040841846 ) ) ;
#4937=DIRECTION ( 'NONE',  ( -1.000000000000000000, -1.224646799147353454E-16, 0.000000000000000000 ) ) ;
#4942=CARTESIAN_POINT ( 'NONE',  ( 0.000000000000000000, 0.000000000000000000, -1.515748031496062964 ) ) ;
#4944=TOROIDAL_SURFACE ( 'NONE', #2362, 0.2952755905511811885, 0.05905511811023622659 ) ;
#4949=VERTEX_POINT ( 'NONE', #6946 ) ;
#4952=DIRECTION ( 'NONE',  ( 1.000000000000000000, 3.472416505924284230E-15, -1.431704036288781660E-14 ) ) ;
#4964=CARTESIAN_POINT ( 'NONE',  ( 0.4338950423154144254, 1.037563309807724821, -1.574803149606299302 ) ) ;
#4967=CARTESIAN_POINT ( 'NONE',  ( 1.037563309807720380, 0.4338950423154246394, -1.574803149606299302 ) ) ;
#4970=CARTESIAN_POINT ( 'NONE',  ( -0.9895441027518994126, 0.4843356560173161518, -1.389133886014302321 ) ) ;
#4976=CARTESIAN_POINT ( 'NONE',  ( 0.8785537298370084125, 0.4700904924197999990, -1.433776001880364470 ) ) ;
#4978=CARTESIAN_POINT ( 'NONE',  ( 0.4700904924197903956, 0.000000000000000000, -2.204724409448820754 ) ) ;
#4983=CARTESIAN_POINT ( 'NONE',  ( 0.9895437626941933074, 0.4843361811957848651, -1.389133361342959949 ) ) ;
#4986=DIRECTION ( 'NONE',  ( -4.632546475182562680E-15, 0.000000000000000000, 1.000000000000000000 ) ) ;
#4987=EDGE_LOOP ( 'NONE', ( #76, #7265, #3139, #5523 ) ) ;
#4988=AXIS2_PLACEMENT_3D ( 'NONE', #7173, #308, #1943 ) ;
#4993=ORIENTED_EDGE ( 'NONE', *, *, #4766, .F. ) ;
#4997=EDGE_CURVE ( 'NONE', #2089, #2327, #6260, .T. ) ;
#5004=CARTESIAN_POINT ( 'NONE',  ( 0.4388996395293570663, 0.9346850374427945196, -1.455943645409046638 ) ) ;
#5008=ORIENTED_EDGE ( 'NONE', *, *, #3793, .F. ) ;
#5012=ORIENTED_EDGE ( 'NONE', *, *, #2854, .F. ) ;
#5016=ADVANCED_FACE ( 'NONE', ( #7018 ), #5773, .F. ) ;
#5018=EDGE_CURVE ( 'NONE', #811, #1871, #3565, .T. ) ;
#5030=B_SPLINE_CURVE_WITH_KNOTS ( 'NONE', 3,
 ( #3122, #4816, #4888, #1986 ),
 .UNSPECIFIED., .F., .F.,
 ( 4, 4 ),
 ( 6.938893903907228378E-18, 0.0002807012396509388046 ),
 .UNSPECIFIED. ) ;
#5041=DIRECTION ( 'NONE',  ( 1.000000000000000000, 1.047067131017167108E-14, 0.000000000000000000 ) ) ;
#5045=CARTESIAN_POINT ( 'NONE',  ( 0.4544645342395077225, 0.9861598787149296053, -1.560495034967182448 ) ) ;
#5046=CIRCLE ( 'NONE', #2337, 1.223643328182681511 ) ;
#5058=CARTESIAN_POINT ( 'NONE',  ( 1.063161309294324175, -0.4348450248026589637, -1.569784497862150907 ) ) ;
#5060=ADVANCED_FACE ( 'NONE', ( #4149 ), #26, .T. ) ;
#5061=EDGE_CURVE ( 'NONE', #2732, #3522, #5412, .T. ) ;
#5063=ORIENTED_EDGE ( 'NONE', *, *, #2578, .T. ) ;
#5068=ORIENTED_EDGE ( 'NONE', *, *, #2199, .T. ) ;
#5069=DIRECTION ( 'NONE',  ( 0.000000000000000000, 0.000000000000000000, -1.000000000000000000 ) ) ;
#5075=CARTESIAN_POINT ( 'NONE',  ( -1.781909941321919274E-15, 0.000000000000000000, -1.397637795275591843 ) ) ;
#5084=FACE_OUTER_BOUND ( 'NONE', #1211, .T. ) ;
#5085=CARTESIAN_POINT ( 'NONE',  ( -0.4700904924197908397, -0.8785537298370134085, -1.433776001880364470 ) ) ;
#5089=DIRECTION ( 'NONE',  ( 0.000000000000000000, 0.000000000000000000, 1.000000000000000000 ) ) ;
#5091=CARTESIAN_POINT ( 'NONE',  ( -0.9984401429152544027, -0.4637690556582386714, -1.410743228759552048 ) ) ;
#5099=FACE_OUTER_BOUND ( 'NONE', #2836, .T. ) ;
#5101=CARTESIAN_POINT ( 'NONE',  ( 0.000000000000000000, 0.000000000000000000, -2.204724409448820754 ) ) ;
#5103=EDGE_CURVE ( 'NONE', #5576, #345, #3449, .T. ) ;
#5106=DIRECTION ( 'NONE',  ( -1.000000000000000000, 0.000000000000000000, 0.000000000000000000 ) ) ;
#5112=CARTESIAN_POINT ( 'NONE',  ( 0.9659644734970493918, 0.4700904924198003876, -1.546597720061112069 ) ) ;
#5118=DIRECTION ( 'NONE',  ( 1.000000000000000000, -1.224646799147353207E-16, 0.000000000000000000 ) ) ;
#5126=CARTESIAN_POINT ( 'NONE',  ( -0.4559220466128923732, -0.8989365377700720972, -1.445239289764782775 ) ) ;
#5133=CARTESIAN_POINT ( 'NONE',  ( -0.2831409772408586822, 0.000000000000000000, -0.8561751947315059397 ) ) ;
#5139=EDGE_LOOP ( 'NONE', ( #1337, #2159, #7350, #128 ) ) ;
#5142=CARTESIAN_POINT ( 'NONE',  ( 0.9696319393316025215, 0.5073702590876725260, -1.367288630522124793 ) ) ;
#5146=VERTEX_POINT ( 'NONE', #7270 ) ;
#5147=B_SPLINE_CURVE_WITH_KNOTS ( 'NONE', 3,
 ( #4714, #632, #4480, #4609, #4037, #7047, #6370, #6480 ),
 .UNSPECIFIED., .F., .F.,
 ( 4, 2, 2, 4 ),
 ( -7.690028535486425530E-06, 0.001102852776893263782, 0.001658124179607642096, 0.002213395582322020411 ),
 .UNSPECIFIED. ) ;
#5149=ORIENTED_EDGE ( 'NONE', *, *, #2388, .T. ) ;
#5155=TOROIDAL_SURFACE ( 'NONE', #6121, 1.124634398195722973, 0.05905511811023622659 ) ;
#5159=CARTESIAN_POINT ( 'NONE',  ( -0.4330708661417317362, 1.048552902599920733, -1.573978973432617279 ) ) ;
#5164=TOROIDAL_SURFACE ( 'NONE', #6883, 1.043121362164705745, 0.05905511811023622659 ) ;
#5166=AXIS2_PLACEMENT_3D ( 'NONE', #418, #2134, #2741 ) ;
#5173=CARTESIAN_POINT ( 'NONE',  ( -0.9883299873891298049, -0.4377664870282987342, -1.443420526770072820 ) ) ;
#5181=CIRCLE ( 'NONE', #1879, 0.9964144355006142595 ) ;
#5195=ADVANCED_FACE ( 'NONE', ( #3451 ), #4793, .T. ) ;
#5199=ADVANCED_FACE ( 'NONE', ( #6250 ), #5543, .T. ) ;
#5200=CARTESIAN_POINT ( 'NONE',  ( -0.8833361873720544377, 0.4663632139996183867, -1.436953241411863313 ) ) ;
#5204=ORIENTED_EDGE ( 'NONE', *, *, #2989, .F. ) ;
#5209=PRODUCT_DEFINITION_FORMATION_WITH_SPECIFIED_SOURCE ( 'ANY', '', #4837, .NOT_KNOWN. ) ;
#5213=CARTESIAN_POINT ( 'NONE',  ( 0.000000000000000000, 0.000000000000000000, 0.000000000000000000 ) ) ;
#5218=CARTESIAN_POINT ( 'NONE',  ( 0.4700904924197906176, 0.9659644734970541657, -1.546597720061111847 ) ) ;
#5221=DIRECTION ( 'NONE',  ( 0.000000000000000000, 0.000000000000000000, -1.000000000000000000 ) ) ;
#5228=FACE_OUTER_BOUND ( 'NONE', #3800, .T. ) ;
#5230=EDGE_CURVE ( 'NONE', #1792, #1409, #3700, .T. ) ;
#5239=ORIENTED_EDGE ( 'NONE', *, *, #1626, .T. ) ;
#5240=EDGE_CURVE ( 'NONE', #6850, #3252, #409, .T. ) ;
#5241=ORIENTED_EDGE ( 'NONE', *, *, #7332, .F. ) ;
#5244=B_SPLINE_CURVE_WITH_KNOTS ( 'NONE', 3,
 ( #4239, #3822, #1510, #4472, #6230, #309, #267, #2027, #4432, #6157 ),
 .UNSPECIFIED., .F., .F.,
 ( 4, 2, 2, 2, 4 ),
 ( 3.469446951953614189E-18, 0.0005494620090385985561, 0.001098924018077193643, 0.001648386027115788730, 0.002197848036154383816 ),
 .UNSPECIFIED. ) ;
#5262=TOROIDAL_SURFACE ( 'NONE', #4167, 1.124634398195722973, 0.05905511811023622659 ) ;
#5266=CARTESIAN_POINT ( 'NONE',  ( 0.4368170415251730332, -0.9411659768779424562, -1.456692913385826849 ) ) ;
#5270=EDGE_LOOP ( 'NONE', ( #330, #56, #289, #5008, #6123 ) ) ;
#5272=EDGE_CURVE ( 'NONE', #4833, #6892, #5290, .T. ) ;
#5274=VERTEX_POINT ( 'NONE', #2158 ) ;
#5276=AXIS2_PLACEMENT_3D ( 'NONE', #4942, #6020, #6124 ) ;
#5278=VERTEX_POINT ( 'NONE', #487 ) ;
#5285=AXIS2_PLACEMENT_3D ( 'NONE', #7046, #3534, #6401 ) ;
#5290=B_SPLINE_CURVE_WITH_KNOTS ( 'NONE', 3,
 ( #2267, #5723, #5823, #7385 ),
 .UNSPECIFIED., .F., .F.,
 ( 4, 4 ),
 ( 0.000000000000000000, 0.0004815725036528569316 ),
 .UNSPECIFIED. ) ;
#5299=CARTESIAN_POINT ( 'NONE',  ( -0.4330708661417322913, -0.9666437042230143772, -1.454455828411337359 ) ) ;
#5304=CARTESIAN_POINT ( 'NONE',  ( 0.4720886891211135694, -0.9960023578760571761, -1.401719942879699143 ) ) ;
#5305=CARTESIAN_POINT ( 'NONE',  ( -0.4637694296357178780, 0.9984400756355462647, -1.410742812766316190 ) ) ;
#5306=CARTESIAN_POINT ( 'NONE',  ( -1.041228047528454104, -0.4333661275892064513, -1.574803149606299302 ) ) ;
#5312=B_SPLINE_CURVE_WITH_KNOTS ( 'NONE', 3,
 ( #6116, #1433, #2630, #4323, #4242, #4932, #1947, #347, #3169, #2065, #875, #1470, #6579, #4970, #4394, #4278, #2518, #196 ),
 .UNSPECIFIED., .F., .F.,
 ( 4, 2, 2, 2, 2, 2, 2, 2, 4 ),
 ( 0.000000000000000000, 0.0002385177155853817146, 0.0004770354311707634292, 0.0009540708623415151491, 0.001431106293512267140, 0.001908141724683019022, 0.002385177155853770471, 0.002862212587024523004, 0.003816283449366010723 ),
 .UNSPECIFIED. ) ;
#5317=EDGE_LOOP ( 'NONE', ( #6701, #1533, #7235, #3302 ) ) ;
#5329=ORIENTED_EDGE ( 'NONE', *, *, #6315, .T. ) ;
#5330=ADVANCED_FACE ( 'NONE', ( #7034 ), #1480, .T. ) ;
#5336=CARTESIAN_POINT ( 'NONE',  ( -1.083410641227607218, 0.4508656291625769419, -1.549345754620972349 ) ) ;
#5337=DIRECTION ( 'NONE',  ( 1.000000000000000000, 1.047444401652940007E-14, 0.000000000000000000 ) ) ;
#5341=CARTESIAN_POINT ( 'NONE',  ( 0.9810556462971108393, 0.4349192958999855696, -1.448591228719269042 ) ) ;
#5346=CARTESIAN_POINT ( 'NONE',  ( -0.4882975260543733764, -0.9867938558989116649, -1.385219839936553177 ) ) ;
#5348=CARTESIAN_POINT ( 'NONE',  ( 0.2831409772408586822, -8.928484287076473300E-17, -0.8561751947315059397 ) ) ;
#5351=DIRECTION ( 'NONE',  ( -1.000000000000000000, 0.000000000000000000, 0.000000000000000000 ) ) ;
#5359=AXIS2_PLACEMENT_3D ( 'NONE', #4201, #1240, #686 ) ;
#5365=DIRECTION ( 'NONE',  ( 1.047444401652940007E-14, -1.000000000000000000, 4.625929269271482167E-15 ) ) ;
#5370=CARTESIAN_POINT ( 'NONE',  ( 1.064252964791707168, -0.5072158114884506297, -1.491281854710054811 ) ) ;
#5374=EDGE_CURVE ( 'NONE', #6357, #1882, #5046, .T. ) ;
#5380=CARTESIAN_POINT ( 'NONE',  ( -1.056523642887404968, 0.5141614760841421994, -1.484898342931014525 ) ) ;
#5382=EDGE_CURVE ( 'NONE', #5648, #1882, #4928, .T. ) ;
#5383=EDGE_CURVE ( 'NONE', #5720, #4020, #3208, .T. ) ;
#5385=CARTESIAN_POINT ( 'NONE',  ( -0.4476001829033103285, 0.9971724964169985661, -1.429776958199370451 ) ) ;
#5388=CARTESIAN_POINT ( 'NONE',  ( 1.081428707249763699, 0.4470331066955068322, -1.553789012478534737 ) ) ;
#5391=B_SPLINE_CURVE_WITH_KNOTS ( 'NONE', 3,
 ( #2627, #7284, #157, #5969 ),
 .UNSPECIFIED., .F., .F.,
 ( 4, 4 ),
 ( 0.000000000000000000, 0.0002807012396509390756 ),
 .UNSPECIFIED. ) ;
#5392=FACE_OUTER_BOUND ( 'NONE', #5270, .T. ) ;
#5395=ORIENTED_EDGE ( 'NONE', *, *, #5230, .F. ) ;
#5400=CIRCLE ( 'NONE', #4900, 1.089828288828796676 ) ;
#5403=CARTESIAN_POINT ( 'NONE',  ( 0.2362204724409449341, 0.000000000000000000, -3.582716535433073002 ) ) ;
#5406=ORIENTED_EDGE ( 'NONE', *, *, #6965, .F. ) ;
#5408=CARTESIAN_POINT ( 'NONE',  ( 0.4330708661417322913, 0.000000000000000000, -2.204724409448820754 ) ) ;
#5409=CIRCLE ( 'NONE', #2828, 0.2362204724409449341 ) ;
#5412=CIRCLE ( 'NONE', #7353, 1.074277634097406953 ) ;
#5413=CARTESIAN_POINT ( 'NONE',  ( -0.9659644734970558311, 0.4700904924197872314, -1.546597720061112069 ) ) ;
#5418=CARTESIAN_POINT ( 'NONE',  ( 1.070877566692234328, -0.4996355910473124773, -1.498503231159224791 ) ) ;
#5420=AXIS2_PLACEMENT_3D ( 'NONE', #2029, #5439, #4356 ) ;
#5433=CARTESIAN_POINT ( 'NONE',  ( 1.070877566692223892, 0.4996355910473349038, -1.498503231159224791 ) ) ;
#5439=DIRECTION ( 'NONE',  ( 1.047444401652940007E-14, -1.000000000000000000, 0.000000000000000000 ) ) ;
#5456=CARTESIAN_POINT ( 'NONE',  ( 1.084813347358868363, -0.4713815370807298843, -1.526966122205014598 ) ) ;
#5462=CARTESIAN_POINT ( 'NONE',  ( -1.051607547633159445, 0.4330708661417285721, -1.573502280244651441 ) ) ;
#5467=CARTESIAN_POINT ( 'NONE',  ( 0.8989365377700750948, -0.4559220466128829363, -1.445239289764781665 ) ) ;
#5479=EDGE_CURVE ( 'NONE', #1792, #6137, #1638, .T. ) ;
#5491=VERTEX_POINT ( 'NONE', #6166 ) ;
#5494=ORIENTED_EDGE ( 'NONE', *, *, #2578, .F. ) ;
#5496=EDGE_LOOP ( 'NONE', ( #2690, #2790, #3518, #3153, #2177, #4658 ) ) ;
#5500=AXIS2_PLACEMENT_3D ( 'NONE', #4557, #6890, #6346 ) ;
#5503=CARTESIAN_POINT ( 'NONE',  ( -0.9659644734970528335, -0.4700904924197936707, -1.546597720061111847 ) ) ;
#5505=CARTESIAN_POINT ( 'NONE',  ( 0.4589124540220939630, -1.085572738833920692, -1.540322878613942681 ) ) ;
#5509=CARTESIAN_POINT ( 'NONE',  ( -0.2362204724409449341, 2.892866454678787531E-17, -0.7983802283864780414 ) ) ;
#5513=ORIENTED_EDGE ( 'NONE', *, *, #7418, .F. ) ;
#5515=CARTESIAN_POINT ( 'NONE',  ( 0.000000000000000000, 0.000000000000000000, -1.484898342931014303 ) ) ;
#5521=ADVANCED_FACE ( 'NONE', ( #1521 ), #6263, .T. ) ;
#5522=CARTESIAN_POINT ( 'NONE',  ( 0.4756000659977976941, 1.083679028610379680, -1.522578585053778744 ) ) ;
#5523=ORIENTED_EDGE ( 'NONE', *, *, #2199, .F. ) ;
#5524=CARTESIAN_POINT ( 'NONE',  ( 0.4541662050560835162, -0.9857970000181582870, -1.560880783937514504 ) ) ;
#5526=EDGE_LOOP ( 'NONE', ( #2903, #3529, #5012, #3782, #5691, #1379, #2612 ) ) ;
#5528=B_SPLINE_CURVE_WITH_KNOTS ( 'NONE', 3,
 ( #5085, #7402, #3937, #5126, #6563, #180, #1180, #7011, #1761, #3530 ),
 .UNSPECIFIED., .F., .F.,
 ( 4, 2, 2, 2, 4 ),
 ( -7.765797721848017974E-06, 0.0005114169989440522576, 0.001030599795609952584, 0.001549782592275852910, 0.002068965388941753237 ),
 .UNSPECIFIED. ) ;
#5532=EDGE_CURVE ( 'NONE', #1492, #383, #6150, .T. ) ;
#5534=VERTEX_POINT ( 'NONE', #3214 ) ;
#5542=EDGE_CURVE ( 'NONE', #1972, #630, #4185, .T. ) ;
#5543=TOROIDAL_SURFACE ( 'NONE', #1368, 1.124634398195722973, 0.05905511811023622659 ) ;
#5547=CARTESIAN_POINT ( 'NONE',  ( 0.4348450093584661502, -1.063161251382698680, -1.569784523562343770 ) ) ;
#5551=CARTESIAN_POINT ( 'NONE',  ( 0.9659644734970590507, -0.4700904924197804591, -1.546597720061111847 ) ) ;
#5555=CARTESIAN_POINT ( 'NONE',  ( -0.4332776171645011942, 1.054581729003112756, -1.572814845875644574 ) ) ;
#5559=TOROIDAL_SURFACE ( 'NONE', #1640, 1.223643328182682621, 0.05905511811023622659 ) ;
#5560=DIRECTION ( 'NONE',  ( 3.491481338843133750E-15, -1.000000000000000000, -4.625929269271482167E-15 ) ) ;
#5567=CARTESIAN_POINT ( 'NONE',  ( 0.9984400756355412687, 0.4637694296357287582, -1.410742812766315746 ) ) ;
#5570=EDGE_LOOP ( 'NONE', ( #1852, #5782, #2494, #3108 ) ) ;
#5572=FACE_OUTER_BOUND ( 'NONE', #2717, .T. ) ;
#5576=VERTEX_POINT ( 'NONE', #2146 ) ;
#5579=CARTESIAN_POINT ( 'NONE',  ( -0.5141614760841463072, 0.9609181420092333115, -1.361499588670821659 ) ) ;
#5589=CARTESIAN_POINT ( 'NONE',  ( 1.037563309807729262, -0.4338950423154036007, -1.574803149606299302 ) ) ;
#5594=SPHERICAL_SURFACE ( 'NONE', #1886, 1.377952755905511806 ) ;
#5599=DIRECTION ( 'NONE',  ( 1.047444401652940007E-14, -1.000000000000000000, 0.000000000000000000 ) ) ;
#5607=CARTESIAN_POINT ( 'NONE',  ( 0.4700904924197906176, -0.9659644734970541657, -1.546597720061111847 ) ) ;
#5612=FACE_OUTER_BOUND ( 'NONE', #3205, .T. ) ;
#5624=CARTESIAN_POINT ( 'NONE',  ( 0.4921259842519683514, 0.000000000000000000, -2.204724409448820754 ) ) ;
#5643=CIRCLE ( 'NONE', #1836, 1.124634398195722973 ) ;
#5648=VERTEX_POINT ( 'NONE', #3012 ) ;
#5654=DIRECTION ( 'NONE',  ( -1.000000000000000000, -0.000000000000000000, -4.625929269271482167E-15 ) ) ;
#5656=CIRCLE ( 'NONE', #2332, 0.2362204724409449341 ) ;
#5663=CARTESIAN_POINT ( 'NONE',  ( 0.4659838021912668382, 0.9705345056684758775, -1.550372027848113010 ) ) ;
#5666=CIRCLE ( 'NONE', #6754, 1.074277634097407175 ) ;
#5668=CARTESIAN_POINT ( 'NONE',  ( 0.000000000000000000, 0.000000000000000000, -2.204724409448820754 ) ) ;
#5670=AXIS2_PLACEMENT_3D ( 'NONE', #7141, #3672, #6011 ) ;
#5671=CARTESIAN_POINT ( 'NONE',  ( 0.4330708661417321803, -0.9697097640641195726, -1.453662949853142594 ) ) ;
#5672=EDGE_CURVE ( 'NONE', #135, #6850, #6474, .T. ) ;
#5677=CARTESIAN_POINT ( 'NONE',  ( -0.9960023578760569540, -0.4720886891211169001, -1.401719942879701364 ) ) ;
#5680=B_SPLINE_CURVE_WITH_KNOTS ( 'NONE', 3,
 ( #3473, #991, #2164, #4044, #7510, #6309, #3944, #1598, #5200, #4616 ),
 .UNSPECIFIED., .F., .F.,
 ( 4, 2, 2, 2, 4 ),
 ( 0.000000000000000000, 0.0005216184974661242351, 0.001043236994932248470, 0.001564855492398372705, 0.002086473989864496940 ),
 .UNSPECIFIED. ) ;
#5685=TOROIDAL_SURFACE ( 'NONE', #3472, 0.2952755905511811885, 0.05905511811023622659 ) ;
#5687=DIRECTION ( 'NONE',  ( -2.207829878515936732E-15, 0.000000000000000000, 1.000000000000000000 ) ) ;
#5691=ORIENTED_EDGE ( 'NONE', *, *, #6556, .F. ) ;
#5700=CARTESIAN_POINT ( 'NONE',  ( 0.9609181420092369752, -0.5141614760841358711, -1.361499588670819216 ) ) ;
#5701=B_SPLINE_CURVE_WITH_KNOTS ( 'NONE', 3,
 ( #341, #2095, #3084, #4964 ),
 .UNSPECIFIED., .F., .F.,
 ( 4, 4 ),
 ( 0.000000000000000000, 0.0002807012396509386419 ),
 .UNSPECIFIED. ) ;
#5702=DIRECTION ( 'NONE',  ( 0.000000000000000000, 0.000000000000000000, -1.000000000000000000 ) ) ;
#5708=CARTESIAN_POINT ( 'NONE',  ( 6.221505307624544299E-30, -1.781909941321919274E-15, -1.397637795275591843 ) ) ;
#5713=CARTESIAN_POINT ( 'NONE',  ( 1.054581729003116530, -0.4332776171644905916, -1.572814845875644352 ) ) ;
#5720=VERTEX_POINT ( 'NONE', #3629 ) ;
#5723=CARTESIAN_POINT ( 'NONE',  ( 0.9604263920613147487, 0.4330708661417422833, -1.456063616177416087 ) ) ;
#5726=( GEOMETRIC_REPRESENTATION_CONTEXT ( 3 ) GLOBAL_UNCERTAINTY_ASSIGNED_CONTEXT ( ( #6337 ) ) GLOBAL_UNIT_ASSIGNED_CONTEXT ( ( #4455, #251, #6855 ) ) REPRESENTATION_CONTEXT ( 'NONE', 'WORKASPACE' ) );
#5727=ORIENTED_EDGE ( 'NONE', *, *, #7058, .F. ) ;
#5728=FACE_OUTER_BOUND ( 'NONE', #3409, .T. ) ;
#5735=TOROIDAL_SURFACE ( 'NONE', #3275, 1.223643328182681289, 0.05905511811023622659 ) ;
#5743=FACE_OUTER_BOUND ( 'NONE', #3795, .T. ) ;
#5744=DIRECTION ( 'NONE',  ( -2.312579046053608732E-29, 2.207829878515936732E-15, 1.000000000000000000 ) ) ;
#5752=AXIS2_PLACEMENT_3D ( 'NONE', #4675, #667, #4099 ) ;
#5753=EDGE_CURVE ( 'NONE', #6423, #6850, #3825, .T. ) ;
#5761=EDGE_CURVE ( 'NONE', #4433, #1688, #3572, .T. ) ;
#5768=DIRECTION ( 'NONE',  ( 0.000000000000000000, 0.000000000000000000, -1.000000000000000000 ) ) ;
#5773=SPHERICAL_SURFACE ( 'NONE', #2587, 1.259842519685039131 ) ;
#5779=B_SPLINE_CURVE_WITH_KNOTS ( 'NONE', 3,
 ( #323, #2726, #2230, #4523 ),
 .UNSPECIFIED., .F., .F.,
 ( 4, 4 ),
 ( 0.000000000000000000, 0.0004815725036528541126 ),
 .UNSPECIFIED. ) ;
#5782=ORIENTED_EDGE ( 'NONE', *, *, #1924, .F. ) ;
#5787=CIRCLE ( 'NONE', #4785, 1.168853328413308690 ) ;
#5791=EDGE_CURVE ( 'NONE', #7462, #345, #5312, .T. ) ;
#5793=EDGE_LOOP ( 'NONE', ( #5063, #3421, #1910, #5861 ) ) ;
#5803=EDGE_CURVE ( 'NONE', #3252, #477, #6874, .T. ) ;
#5809=EDGE_CURVE ( 'NONE', #5935, #408, #1487, .T. ) ;
#5815=DIRECTION ( 'NONE',  ( 2.312579046053608732E-29, -2.207829878515936732E-15, -1.000000000000000000 ) ) ;
#5821=DIRECTION ( 'NONE',  ( -1.000000000000000000, 1.224646799147353207E-16, 0.000000000000000000 ) ) ;
#5823=CARTESIAN_POINT ( 'NONE',  ( 0.9541934910893004052, 0.4339190921229551523, -1.456692913385828847 ) ) ;
#5826=CARTESIAN_POINT ( 'NONE',  ( -0.9917530546321610130, 0.4509662133831486841, -1.563429817131423372 ) ) ;
#5840=CARTESIAN_POINT ( 'NONE',  ( -0.9604263920613191896, 0.4330708661417286276, -1.456063616177414310 ) ) ;
#5841=CARTESIAN_POINT ( 'NONE',  ( -0.4330708661417322913, 0.9697097892794930285, -1.453662943332487023 ) ) ;
#5843=TOROIDAL_SURFACE ( 'NONE', #356, 1.223643328182682621, 0.05905511811023622659 ) ;
#5844=EDGE_CURVE ( 'NONE', #3756, #3765, #168, .T. ) ;
#5850=EDGE_CURVE ( 'NONE', #4833, #6826, #2952, .T. ) ;
#5858=ORIENTED_EDGE ( 'NONE', *, *, #2891, .T. ) ;
#5860=FACE_OUTER_BOUND ( 'NONE', #2148, .T. ) ;
#5861=ORIENTED_EDGE ( 'NONE', *, *, #5018, .F. ) ;
#5874=CARTESIAN_POINT ( 'NONE',  ( -1.054581703806072746, 0.4332776154273863534, -1.572814851683855819 ) ) ;
#5875=CARTESIAN_POINT ( 'NONE',  ( 0.000000000000000000, 0.000000000000000000, -2.204724409448820754 ) ) ;
#5879=CARTESIAN_POINT ( 'NONE',  ( -0.2362204724409449341, 2.892866454678787531E-17, -3.582716535433073002 ) ) ;
#5880=CARTESIAN_POINT ( 'NONE',  ( -0.4999746636856473581, 0.9773775067402683536, -1.373988502838981107 ) ) ;
#5883=CARTESIAN_POINT ( 'NONE',  ( 1.075170037517928723, 0.4403525121893840932, -1.561970602951606946 ) ) ;
#5898=AXIS2_PLACEMENT_3D ( 'NONE', #6053, #3783, #6085 ) ;
#5906=CIRCLE ( 'NONE', #6517, 1.074277634097406953 ) ;
#5912=CARTESIAN_POINT ( 'NONE',  ( -1.070877820178675721, -0.4996352642496130203, -1.498503547059352181 ) ) ;
#5919=CARTESIAN_POINT ( 'NONE',  ( 1.037563309807720380, 0.4338950423154246394, -1.574803149606299302 ) ) ;
#5920=CARTESIAN_POINT ( 'NONE',  ( 0.000000000000000000, 0.000000000000000000, -1.574803149606299302 ) ) ;
#5924=CARTESIAN_POINT ( 'NONE',  ( 0.4627504720074770983, -0.8884022185686297757, -1.439912370850674028 ) ) ;
#5925=CARTESIAN_POINT ( 'NONE',  ( -1.037563309807723488, -0.4338950423154175340, -1.574803149606299302 ) ) ;
#5928=PRODUCT_DEFINITION ( 'UNKNOWN', '', #5209, #1274 ) ;
#5931=DIRECTION ( 'NONE',  ( 2.204015539012438360E-32, 4.625929269271482167E-15, -1.000000000000000000 ) ) ;
#5933=CARTESIAN_POINT ( 'NONE',  ( -0.4341579012690682804, -1.060348472569315303, -1.570964862939434825 ) ) ;
#5935=VERTEX_POINT ( 'NONE', #7403 ) ;
#5940=B_SPLINE_CURVE_WITH_KNOTS ( 'NONE', 3,
 ( #981, #6685, #5004, #2172, #3274, #3741, #6189, #4390, #910, #7252 ),
 .UNSPECIFIED., .F., .F.,
 ( 4, 2, 2, 2, 4 ),
 ( 0.000000000000000000, 0.0005216184974661249940, 0.001043236994932249988, 0.001564855492398375091, 0.002086473989864499976 ),
 .UNSPECIFIED. ) ;
#5942=CARTESIAN_POINT ( 'NONE',  ( 0.4330708661417322913, 0.9666437042230126009, -1.454455828411335583 ) ) ;
#5950=EDGE_CURVE ( 'NONE', #408, #1972, #650, .T. ) ;
#5951=FACE_OUTER_BOUND ( 'NONE', #4987, .T. ) ;
#5959=CARTESIAN_POINT ( 'NONE',  ( 1.048552902599924730, -0.4330708661417213001, -1.573978973432616835 ) ) ;
#5962=CARTESIAN_POINT ( 'NONE',  ( -0.4349482548737262921, -1.030265823844199069, -1.574803149606299746 ) ) ;
#5969=CARTESIAN_POINT ( 'NONE',  ( 1.037563309807729262, -0.4338950423154036007, -1.574803149606299302 ) ) ;
#5972=CARTESIAN_POINT ( 'NONE',  ( -0.4630669964643905900, -1.085749034322389894, -1.535808346805854541 ) ) ;
#5974=VERTEX_POINT ( 'NONE', #425 ) ;
#5985=AXIS2_PLACEMENT_3D ( 'NONE', #7417, #5687, #3374 ) ;
#5988=FACE_OUTER_BOUND ( 'NONE', #2346, .T. ) ;
#5989=CARTESIAN_POINT ( 'NONE',  ( -0.4353079511162236681, -0.9479499796399322165, -1.456692913385828625 ) ) ;
#5994=ORIENTED_EDGE ( 'NONE', *, *, #7461, .F. ) ;
#5999=AXIS2_PLACEMENT_3D ( 'NONE', #3551, #6544, #727 ) ;
#6000=ADVANCED_FACE ( 'NONE', ( #4585 ), #5164, .T. ) ;
#6002=CARTESIAN_POINT ( 'NONE',  ( -0.9479499796399322165, 0.4353079511162203374, -1.456692913385826849 ) ) ;
#6005=TOROIDAL_SURFACE ( 'NONE', #380, 1.124634398195722973, 0.05905511811023622659 ) ;
#6011=DIRECTION ( 'NONE',  ( -1.000000000000000000, -1.049299683535327448E-14, 0.000000000000000000 ) ) ;
#6013=ORIENTED_EDGE ( 'NONE', *, *, #1931, .T. ) ;
#6020=DIRECTION ( 'NONE',  ( 0.000000000000000000, 0.000000000000000000, -1.000000000000000000 ) ) ;
#6021=ORIENTED_EDGE ( 'NONE', *, *, #2711, .T. ) ;
#6028=CARTESIAN_POINT ( 'NONE',  ( -0.4700904924197908397, -0.8785537298370134085, -1.433776001880364470 ) ) ;
#6030=ORIENTED_EDGE ( 'NONE', *, *, #2891, .F. ) ;
#6031=AXIS2_PLACEMENT_3D ( 'NONE', #4978, #7297, #3834 ) ;
#6039=CARTESIAN_POINT ( 'NONE',  ( -0.8833138556570234723, -0.4663806185493133416, -1.436938405272265573 ) ) ;
#6043=DIRECTION ( 'NONE',  ( 0.000000000000000000, 0.000000000000000000, -1.000000000000000000 ) ) ;
#6053=CARTESIAN_POINT ( 'NONE',  ( -0.4700904924197872314, 0.000000000000000000, -2.204724409448822975 ) ) ;
#6054=CARTESIAN_POINT ( 'NONE',  ( -0.4375700573520698300, 1.070856907295305804, -1.565644078513316106 ) ) ;
#6055=APPLICATION_CONTEXT ( 'automotive_design' ) ;
#6066=CARTESIAN_POINT ( 'NONE',  ( 0.9883301303667366700, -0.4377665650305532230, -1.443420399700354295 ) ) ;
#6067=ORIENTED_EDGE ( 'NONE', *, *, #5950, .F. ) ;
#6070=DIRECTION ( 'NONE',  ( -1.776356839400250465E-15, 1.000000000000000000, -2.256009703088257329E-15 ) ) ;
#6073=CARTESIAN_POINT ( 'NONE',  ( 1.037563309807729262, -0.4338950423154036007, -1.574803149606299302 ) ) ;
#6082=FACE_OUTER_BOUND ( 'NONE', #3335, .T. ) ;
#6085=DIRECTION ( 'NONE',  ( 4.615976749461840186E-15, 0.000000000000000000, -1.000000000000000000 ) ) ;
#6086=DIRECTION ( 'NONE',  ( -1.000000000000000000, 0.000000000000000000, 0.000000000000000000 ) ) ;
#6088=DIRECTION ( 'NONE',  ( -0.000000000000000000, -1.000000000000000000, 0.000000000000000000 ) ) ;
#6093=CARTESIAN_POINT ( 'NONE',  ( 0.5072158114890842340, 1.064252964791788658, -1.491281854710626575 ) ) ;
#6100=AXIS2_PLACEMENT_3D ( 'NONE', #2950, #2379, #2993 ) ;
#6110=CARTESIAN_POINT ( 'NONE',  ( -0.8989365377700702098, -0.4559220466128956484, -1.445239289764782997 ) ) ;
#6116=CARTESIAN_POINT ( 'NONE',  ( -0.9666437042230142662, 0.4330708661417289052, -1.454455828411335583 ) ) ;
#6120=DIRECTION ( 'NONE',  ( -1.000000000000000000, 0.000000000000000000, 0.000000000000000000 ) ) ;
#6121=AXIS2_PLACEMENT_3D ( 'NONE', #690, #3013, #5351 ) ;
#6123=ORIENTED_EDGE ( 'NONE', *, *, #4615, .F. ) ;
#6124=DIRECTION ( 'NONE',  ( -1.000000000000000000, 0.000000000000000000, 0.000000000000000000 ) ) ;
#6131=EDGE_CURVE ( 'NONE', #630, #443, #5906, .T. ) ;
#6137=VERTEX_POINT ( 'NONE', #6947 ) ;
#6140=ORIENTED_EDGE ( 'NONE', *, *, #1589, .F. ) ;
#6146=B_SPLINE_CURVE_WITH_KNOTS ( 'NONE', 3,
 ( #5989, #1340, #4677, #16 ),
 .UNSPECIFIED., .F., .F.,
 ( 4, 4 ),
 ( 0.000000000000000000, 0.0004815725036528575279 ),
 .UNSPECIFIED. ) ;
#6150=CIRCLE ( 'NONE', #2343, 1.223643328182681289 ) ;
#6154=DIRECTION ( 'NONE',  ( 7.708596820178695308E-30, -2.207829878515936732E-15, 1.000000000000000000 ) ) ;
#6157=CARTESIAN_POINT ( 'NONE',  ( -0.4700904924197902846, 0.9659644734970543878, -1.546597720061111847 ) ) ;
#6159=B_SPLINE_CURVE_WITH_KNOTS ( 'NONE', 3,
 ( #2437, #4770, #5433, #4156, #4236, #7106, #189, #2511, #7209, #6497, #5388, #5883, #4844, #1866, #7170, #4272, #6610, #67 ),
 .UNSPECIFIED., .F., .F.,
 ( 4, 2, 2, 2, 2, 2, 2, 2, 4 ),
 ( -8.042425861379543572E-06, 0.0009212656149224119229, 0.001385919635314298778, 0.001850573655706185634, 0.002315227676098072923, 0.002779881696489959562, 0.003244535716881846200, 0.003476862727077784532, 0.003709189737273723732 ),
 .UNSPECIFIED. ) ;
#6163=VECTOR ( 'NONE', #755, 39.37007874015748143 ) ;
#6164=CARTESIAN_POINT ( 'NONE',  ( 0.4375700573520702741, 1.070856907295305804, -1.565644078513316773 ) ) ;
#6166=CARTESIAN_POINT ( 'NONE',  ( 0.5141614760841458631, 1.056523642887403192, -1.484898342931014303 ) ) ;
#6167=ORIENTED_EDGE ( 'NONE', *, *, #7191, .T. ) ;
#6168=ORIENTED_EDGE ( 'NONE', *, *, #4997, .F. ) ;
#6173=CARTESIAN_POINT ( 'NONE',  ( 0.9810556462971189440, -0.4349192958999650305, -1.448591228719267487 ) ) ;
#6177=ORIENTED_EDGE ( 'NONE', *, *, #5542, .F. ) ;
#6180=EDGE_CURVE ( 'NONE', #4020, #7296, #117, .T. ) ;
#6187=CARTESIAN_POINT ( 'NONE',  ( 0.4368380215374126352, 1.023371766162644914, -1.573834103987475475 ) ) ;
#6189=CARTESIAN_POINT ( 'NONE',  ( 0.4559215864680338792, 0.8989373009621102195, -1.445239633971734383 ) ) ;
#6191=DIRECTION ( 'NONE',  ( 1.000000000000000000, 1.047444401652940007E-14, 0.000000000000000000 ) ) ;
#6195=ORIENTED_EDGE ( 'NONE', *, *, #1536, .F. ) ;
#6196=LINE ( 'NONE', #5879, #6163 ) ;
#6202=ORIENTED_EDGE ( 'NONE', *, *, #6492, .T. ) ;
#6204=ORIENTED_EDGE ( 'NONE', *, *, #2855, .T. ) ;
#6207=ORIENTED_EDGE ( 'NONE', *, *, #1589, .T. ) ;
#6212=B_SPLINE_CURVE_WITH_KNOTS ( 'NONE', 3,
 ( #5925, #5306, #2436, #2922 ),
 .UNSPECIFIED., .F., .F.,
 ( 4, 4 ),
 ( 6.648767611728001586E-17, 0.0002807012396508847571 ),
 .UNSPECIFIED. ) ;
#6223=EDGE_CURVE ( 'NONE', #2089, #4463, #3113, .T. ) ;
#6225=CARTESIAN_POINT ( 'NONE',  ( 0.4445641707282979582, 1.003668447264491226, -1.568529612473645862 ) ) ;
#6226=AXIS2_PLACEMENT_3D ( 'NONE', #47, #5365, #6471 ) ;
#6230=CARTESIAN_POINT ( 'NONE',  ( -0.4445641707282975696, 1.003668447264491226, -1.568529612473645418 ) ) ;
#6238=CARTESIAN_POINT ( 'NONE',  ( -0.9773781006402562088, -0.4999740374263574871, -1.373989084484001477 ) ) ;
#6244=CARTESIAN_POINT ( 'NONE',  ( 0.9971724964169936811, 0.4476001829033208201, -1.429776958199370451 ) ) ;
#6246=ORIENTED_EDGE ( 'NONE', *, *, #4664, .T. ) ;
#6248=ORIENTED_EDGE ( 'NONE', *, *, #4146, .F. ) ;
#6250=FACE_OUTER_BOUND ( 'NONE', #7119, .T. ) ;
#6258=CARTESIAN_POINT ( 'NONE',  ( 0.8785537298370084125, 0.4700904924197999990, -1.433776001880364470 ) ) ;
#6260=CIRCLE ( 'NONE', #2943, 0.9964144355006142595 ) ;
#6263=TOROIDAL_SURFACE ( 'NONE', #5276, 1.124634398195722973, 0.05905511811023622659 ) ;
#6265=CARTESIAN_POINT ( 'NONE',  ( 0.2362204724409449341, 0.000000000000000000, 0.000000000000000000 ) ) ;
#6268=CARTESIAN_POINT ( 'NONE',  ( -1.702122929023921302E-15, 0.000000000000000000, -1.433776001880364026 ) ) ;
#6271=CARTESIAN_POINT ( 'NONE',  ( 0.000000000000000000, 0.000000000000000000, -1.515748031496062964 ) ) ;
#6272=DIRECTION ( 'NONE',  ( 6.217248937900876626E-15, 1.000000000000000000, -2.256009703088257329E-15 ) ) ;
#6275=ADVANCED_FACE ( 'NONE', ( #7397 ), #3444, .T. ) ;
#6276=DIRECTION ( 'NONE',  ( -1.000000000000000000, -0.000000000000000000, -4.625929269271482167E-15 ) ) ;
#6285=CARTESIAN_POINT ( 'NONE',  ( 0.000000000000000000, 0.000000000000000000, -1.484898342931014303 ) ) ;
#6291=ORIENTED_EDGE ( 'NONE', *, *, #7513, .F. ) ;
#6292=DIMENSIONAL_EXPONENTS ( 1.000000000000000000, 0.000000000000000000, 0.000000000000000000, 0.000000000000000000, 0.000000000000000000, 0.000000000000000000, 0.000000000000000000 ) ;
#6294=CARTESIAN_POINT ( 'NONE',  ( 0.5141614760841460852, -0.9609181420092316461, -1.361499588670819216 ) ) ;
#6301=B_SPLINE_CURVE_WITH_KNOTS ( 'NONE', 3,
 ( #3666, #3818, #833, #5467, #3239, #1019, #7474, #58, #3535, #1229 ),
 .UNSPECIFIED., .F., .F.,
 ( 4, 2, 2, 2, 4 ),
 ( -7.765797721857259104E-06, 0.0005114169989440442345, 0.001030599795609945862, 0.001549782592275847273, 0.002068965388941748900 ),
 .UNSPECIFIED. ) ;
#6306=EDGE_CURVE ( 'NONE', #3522, #2089, #5787, .T. ) ;
#6309=CARTESIAN_POINT ( 'NONE',  ( -0.9044351468059373955, 0.4526810454163289199, -1.447629383090422772 ) ) ;
#6311=CARTESIAN_POINT ( 'NONE',  ( -0.4332839536939404601, -0.9726683636255534227, -1.452651081959920765 ) ) ;
#6315=EDGE_CURVE ( 'NONE', #4054, #2045, #35, .T. ) ;
#6323=ORIENTED_EDGE ( 'NONE', *, *, #2252, .T. ) ;
#6324=CARTESIAN_POINT ( 'NONE',  ( 0.5141614760841457521, 0.000000000000000000, -2.204724409448820754 ) ) ;
#6327=ORIENTED_EDGE ( 'NONE', *, *, #4435, .T. ) ;
#6333=AXIS2_PLACEMENT_3D ( 'NONE', #3124, #231, #2552 ) ;
#6335=AXIS2_PLACEMENT_3D ( 'NONE', #3547, #1944, #761 ) ;
#6337=UNCERTAINTY_MEASURE_WITH_UNIT (LENGTH_MEASURE( 1.000000000000000082E-05 ), #4455, 'distance_accuracy_value', 'NONE');
#6339=TOROIDAL_SURFACE ( 'NONE', #5985, 1.043121362164705745, 0.05905511811023622659 ) ;
#6340=CARTESIAN_POINT ( 'NONE',  ( 0.4514963146295077334, -0.9983958463931797978, -1.424958914991359960 ) ) ;
#6344=CARTESIAN_POINT ( 'NONE',  ( -0.4377664870282949594, -0.9883299873891312481, -1.443420526770072598 ) ) ;
#6346=DIRECTION ( 'NONE',  ( 0.000000000000000000, 1.000000000000000000, 2.256009703088257329E-15 ) ) ;
#6357=VERTEX_POINT ( 'NONE', #3851 ) ;
#6359=CARTESIAN_POINT ( 'NONE',  ( -1.010073413237867923, 0.4416276115803053348, -1.570717210673254538 ) ) ;
#6361=ORIENTED_EDGE ( 'NONE', *, *, #986, .T. ) ;
#6365=CIRCLE ( 'NONE', #3677, 0.05905511811023627516 ) ;
#6370=CARTESIAN_POINT ( 'NONE',  ( -1.030265823844197293, -0.4349482548737299559, -1.574803149606299302 ) ) ;
#6374=CARTESIAN_POINT ( 'NONE',  ( 5.942930443104038687E-30, -1.702122929023921893E-15, -1.433776001880363582 ) ) ;
#6381=ORIENTED_EDGE ( 'NONE', *, *, #5103, .T. ) ;
#6383=CARTESIAN_POINT ( 'NONE',  ( -0.9964144355006142595, 1.220255749060045517E-16, -1.433776001880363360 ) ) ;
#6388=ORIENTED_EDGE ( 'NONE', *, *, #5103, .F. ) ;
#6389=DIRECTION ( 'NONE',  ( 0.000000000000000000, 0.000000000000000000, 1.000000000000000000 ) ) ;
#6396=EDGE_CURVE ( 'NONE', #5974, #1691, #3198, .T. ) ;
#6399=CARTESIAN_POINT ( 'NONE',  ( 1.056523642887408521, -0.5141614760841347609, -1.484898342931014303 ) ) ;
#6401=DIRECTION ( 'NONE',  ( 1.765631543889772066E-46, -1.000000000000000000, -2.207829878515936732E-15 ) ) ;
#6402=ADVANCED_FACE ( 'NONE', ( #4426 ), #1016, .T. ) ;
#6404=( NAMED_UNIT ( * ) SI_UNIT ( $, .STERADIAN. ) SOLID_ANGLE_UNIT ( ) );
#6410=CARTESIAN_POINT ( 'NONE',  ( 0.4526814320286470794, -0.9044344578135156132, -1.447629106959917200 ) ) ;
#6415=CARTESIAN_POINT ( 'NONE',  ( -0.4837908950006660214, -1.080458485393811952, -1.514208454829283790 ) ) ;
#6417=ORIENTED_EDGE ( 'NONE', *, *, #6396, .F. ) ;
#6423=VERTEX_POINT ( 'NONE', #4642 ) ;
#6428=ORIENTED_EDGE ( 'NONE', *, *, #1767, .F. ) ;
#6429=CARTESIAN_POINT ( 'NONE',  ( -1.782879132931211256E-29, 1.702122929023921696E-15, -1.433776001880364026 ) ) ;
#6434=CARTESIAN_POINT ( 'NONE',  ( -1.085572738833919360, -0.4589124540220979043, -1.540322878613942903 ) ) ;
#6439=ORIENTED_EDGE ( 'NONE', *, *, #5018, .T. ) ;
#6445=DIRECTION ( 'NONE',  ( -0.000000000000000000, -0.000000000000000000, 1.000000000000000000 ) ) ;
#6449=DIRECTION ( 'NONE',  ( -1.000000000000000000, 0.000000000000000000, 0.000000000000000000 ) ) ;
#6453=CARTESIAN_POINT ( 'NONE',  ( -1.729881963583410815E-29, 1.651526287078852914E-15, -1.456692913385827515 ) ) ;
#6456=CARTESIAN_POINT ( 'NONE',  ( -0.4755998196564488745, -1.083679103503828456, -1.522578840002906997 ) ) ;
#6458=AXIS2_PLACEMENT_3D ( 'NONE', #5668, #3166, #423 ) ;
#6459=ORIENTED_EDGE ( 'NONE', *, *, #2887, .F. ) ;
#6460=ORIENTED_EDGE ( 'NONE', *, *, #571, .T. ) ;
#6470=DIRECTION ( 'NONE',  ( 0.000000000000000000, 1.000000000000000000, -2.193342766891360832E-15 ) ) ;
#6471=DIRECTION ( 'NONE',  ( 1.000000000000000000, 1.045898529308442724E-14, 0.000000000000000000 ) ) ;
#6474=B_SPLINE_CURVE_WITH_KNOTS ( 'NONE', 3,
 ( #4121, #36, #1873, #5933, #73, #573, #2358, #3591, #2319, #2972, #5972, #2444, #6456, #6415, #4085, #3511, #1054, #116 ),
 .UNSPECIFIED., .F., .F.,
 ( 4, 2, 2, 2, 2, 2, 2, 2, 4 ),
 ( 0.000000000000000000, 0.0002327816859446661863, 0.0004655633718893323727, 0.0009311267437786552043, 0.001396690115667977928, 0.001862253487557300868, 0.002327816859446623591, 0.002793380231335946314, 0.003724506975114578750 ),
 .UNSPECIFIED. ) ;
#6476=ORIENTED_EDGE ( 'NONE', *, *, #4447, .T. ) ;
#6477=CARTESIAN_POINT ( 'NONE',  ( -1.084813395429186977, -0.4713813068963941810, -1.526966363676887095 ) ) ;
#6478=ORIENTED_EDGE ( 'NONE', *, *, #160, .T. ) ;
#6480=CARTESIAN_POINT ( 'NONE',  ( -1.037563309807723488, -0.4338950423154175340, -1.574803149606299302 ) ) ;
#6481=ORIENTED_EDGE ( 'NONE', *, *, #4073, .T. ) ;
#6484=DIRECTION ( 'NONE',  ( 0.000000000000000000, 0.000000000000000000, -1.000000000000000000 ) ) ;
#6485=CARTESIAN_POINT ( 'NONE',  ( 1.041228047528450995, 0.4333661275892136122, -1.574803149606299302 ) ) ;
#6491=CARTESIAN_POINT ( 'NONE',  ( 0.4762522394722484842, -0.9941399105654876722, -1.397361772547373260 ) ) ;
#6492=EDGE_CURVE ( 'NONE', #1409, #2214, #4424, .T. ) ;
#6495=CARTESIAN_POINT ( 'NONE',  ( 0.5141614760841459741, -1.056523642887403192, -1.484898342931014303 ) ) ;
#6497=CARTESIAN_POINT ( 'NONE',  ( 1.083410700381141289, 0.4508657589754813122, -1.549345605342071552 ) ) ;
#6506=EDGE_LOOP ( 'NONE', ( #6595, #6246, #1306, #1203, #3250, #5395 ) ) ;
#6515=CARTESIAN_POINT ( 'NONE',  ( 0.4762527114670027650, 0.9941396836775473478, -1.397361282224857781 ) ) ;
#6517=AXIS2_PLACEMENT_3D ( 'NONE', #2853, #7508, #4614 ) ;
#6519=FACE_OUTER_BOUND ( 'NONE', #4693, .T. ) ;
#6524=ORIENTED_EDGE ( 'NONE', *, *, #287, .T. ) ;
#6531=DIRECTION ( 'NONE',  ( -2.207829878515936732E-15, 0.000000000000000000, 1.000000000000000000 ) ) ;
#6534=CARTESIAN_POINT ( 'NONE',  ( -0.4416272204090970765, -1.010074371201533205, -1.570717485485533249 ) ) ;
#6535=CARTESIAN_POINT ( 'NONE',  ( 0.9726684123052288244, 0.4332839571663439915, -1.452651065350217596 ) ) ;
#6544=DIRECTION ( 'NONE',  ( 7.708596820178695308E-30, -2.207829878515936732E-15, 1.000000000000000000 ) ) ;
#6550=CARTESIAN_POINT ( 'NONE',  ( 0.4596436929058889120, 0.9990286721055788854, -1.415369458146013226 ) ) ;
#6556=EDGE_CURVE ( 'NONE', #3765, #4054, #3545, .T. ) ;
#6561=DIRECTION ( 'NONE',  ( 0.000000000000000000, 0.000000000000000000, -1.000000000000000000 ) ) ;
#6562=CARTESIAN_POINT ( 'NONE',  ( -1.056523642887401415, -0.5141614760841493048, -1.484898342931014303 ) ) ;
#6563=CARTESIAN_POINT ( 'NONE',  ( -0.4526814320286470794, -0.9044344578135171675, -1.447629106959918754 ) ) ;
#6567=ORIENTED_EDGE ( 'NONE', *, *, #5061, .T. ) ;
#6569=CARTESIAN_POINT ( 'NONE',  ( 0.4508656291625806056, -1.083410641227605664, -1.549345754620972127 ) ) ;
#6571=CARTESIAN_POINT ( 'NONE',  ( -0.9666437042230142662, 0.4330708661417289052, -1.454455828411335583 ) ) ;
#6575=DIRECTION ( 'NONE',  ( -2.207829878515936732E-15, 0.000000000000000000, 1.000000000000000000 ) ) ;
#6576=CARTESIAN_POINT ( 'NONE',  ( 5.154746071126671174E-15, -0.4921259842519683514, -2.204724409448820754 ) ) ;
#6579=CARTESIAN_POINT ( 'NONE',  ( -0.9941399105654891155, 0.4762522394722451535, -1.397361772547373038 ) ) ;
#6583=CARTESIAN_POINT ( 'NONE',  ( 0.4330708661417321803, 1.051607560569805422, -1.573502278225820339 ) ) ;
#6586=CARTESIAN_POINT ( 'NONE',  ( 0.5073702590884642261, 0.9696319393317771596, -1.367288630522805359 ) ) ;
#6590=AXIS2_PLACEMENT_3D ( 'NONE', #5213, #2870, #4668 ) ;
#6591=EDGE_CURVE ( 'NONE', #4474, #1329, #6365, .T. ) ;
#6592=ADVANCED_FACE ( 'NONE', ( #862 ), #1213, .T. ) ;
#6595=ORIENTED_EDGE ( 'NONE', *, *, #5479, .T. ) ;
#6597=ORIENTED_EDGE ( 'NONE', *, *, #298, .F. ) ;
#6601=ORIENTED_EDGE ( 'NONE', *, *, #4289, .T. ) ;
#6606=CARTESIAN_POINT ( 'NONE',  ( 0.4755998196564493741, -1.083679103503828456, -1.522578840002907219 ) ) ;
#6610=CARTESIAN_POINT ( 'NONE',  ( 1.051607560569801425, 0.4330708661417428385, -1.573502278225820783 ) ) ;
#6619=CARTESIAN_POINT ( 'NONE',  ( -0.4368170150760394277, 0.9411660957780404457, -1.456692913385828847 ) ) ;
#6620=ORIENTED_EDGE ( 'NONE', *, *, #4764, .T. ) ;
#6622=SPHERICAL_SURFACE ( 'NONE', #2097, 1.377952755905511806 ) ;
#6626=AXIS2_PLACEMENT_3D ( 'NONE', #4072, #3496, #1225 ) ;
#6627=ORIENTED_EDGE ( 'NONE', *, *, #6913, .T. ) ;
#6631=DIRECTION ( 'NONE',  ( -0.000000000000000000, -0.000000000000000000, 1.000000000000000000 ) ) ;
#6635=ORIENTED_EDGE ( 'NONE', *, *, #160, .F. ) ;
#6644=CARTESIAN_POINT ( 'NONE',  ( 0.4375700189966303388, -1.070856827570678904, -1.565644132322242532 ) ) ;
#6647=DIRECTION ( 'NONE',  ( 1.000000000000000000, 0.000000000000000000, -0.000000000000000000 ) ) ;
#6649=B_SPLINE_CURVE_WITH_KNOTS ( 'NONE', 3,
 ( #7223, #6729, #1998, #4329 ),
 .UNSPECIFIED., .F., .F.,
 ( 4, 4 ),
 ( 3.469446951953614189E-18, 0.0004815725036528502637 ),
 .UNSPECIFIED. ) ;
#6653=DIRECTION ( 'NONE',  ( 0.000000000000000000, -1.000000000000000000, 0.000000000000000000 ) ) ;
#6658=CARTESIAN_POINT ( 'NONE',  ( -0.4403525121893726579, 1.075170037517933386, -1.561970602951606280 ) ) ;
#6666=ORIENTED_EDGE ( 'NONE', *, *, #3184, .T. ) ;
#6672=CARTESIAN_POINT ( 'NONE',  ( 0.9697097892794954710, -0.4330708661417219663, -1.453662943332484803 ) ) ;
#6683=ADVANCED_FACE ( 'NONE', ( #5572 ), #6005, .T. ) ;
#6684=ADVANCED_FACE ( 'NONE', ( #5612 ), #4644, .T. ) ;
#6685=CARTESIAN_POINT ( 'NONE',  ( 0.4368170150760393167, 0.9411660957780392245, -1.456692913385826849 ) ) ;
#6687=ORIENTED_EDGE ( 'NONE', *, *, #459, .T. ) ;
#6689=DIRECTION ( 'NONE',  ( -2.207829878515936732E-15, 0.000000000000000000, 1.000000000000000000 ) ) ;
#6697=CARTESIAN_POINT ( 'NONE',  ( -0.4353079511162236681, 0.9479499796399324385, -1.456692913385828625 ) ) ;
#6701=ORIENTED_EDGE ( 'NONE', *, *, #382, .T. ) ;
#6703=CIRCLE ( 'NONE', #6335, 1.124634398195722973 ) ;
#6704=CARTESIAN_POINT ( 'NONE',  ( -1.048552902599921843, 0.4330708661417285721, -1.573978973432616835 ) ) ;
#6706=CARTESIAN_POINT ( 'NONE',  ( 0.9783381746514295818, -0.4342019027940097198, -1.450123259817208909 ) ) ;
#6716=CARTESIAN_POINT ( 'NONE',  ( 0.4630669964643910341, -1.085749034322389672, -1.535808346805854541 ) ) ;
#6721=CARTESIAN_POINT ( 'NONE',  ( 0.9857970000181629500, -0.4541662050560733577, -1.560880783937514504 ) ) ;
#6722=CARTESIAN_POINT ( 'NONE',  ( 0.9705345056685881211, 0.4659838021921174356, -1.550372027848885281 ) ) ;
#6729=CARTESIAN_POINT ( 'NONE',  ( 0.4339190921229451048, 0.9541934910893031807, -1.456692913385826849 ) ) ;
#6733=EDGE_CURVE ( 'NONE', #7028, #2144, #2699, .T. ) ;
#6736=ORIENTED_EDGE ( 'NONE', *, *, #1536, .T. ) ;
#6740=CARTESIAN_POINT ( 'NONE',  ( 0.9941396836775518997, -0.4762527114669922734, -1.397361282224856671 ) ) ;
#6754=AXIS2_PLACEMENT_3D ( 'NONE', #419, #4316, #4469 ) ;
#6758=AXIS2_PLACEMENT_3D ( 'NONE', #945, #1052, #5118 ) ;
#6766=CARTESIAN_POINT ( 'NONE',  ( -0.4330708661417317362, -1.048552902599920955, -1.573978973432617279 ) ) ;
#6768=AXIS2_PLACEMENT_3D ( 'NONE', #6271, #3397, #4550 ) ;
#6771=CARTESIAN_POINT ( 'NONE',  ( -0.9666437042230129340, -0.4330708661417356220, -1.454455828411337359 ) ) ;
#6773=CARTESIAN_POINT ( 'NONE',  ( 1.075170037517937605, -0.4403525121893617778, -1.561970602951606946 ) ) ;
#6779=CARTESIAN_POINT ( 'NONE',  ( 0.9960021845704828403, 0.4720891361949586806, -1.401719468380313360 ) ) ;
#6781=EDGE_CURVE ( 'NONE', #75, #3031, #5643, .T. ) ;
#6785=DIRECTION ( 'NONE',  ( -1.000000000000000000, -0.000000000000000000, -4.625929269271482167E-15 ) ) ;
#6788=DIRECTION ( 'NONE',  ( -1.000000000000000000, 0.000000000000000000, 0.000000000000000000 ) ) ;
#6789=ORIENTED_EDGE ( 'NONE', *, *, #1200, .F. ) ;
#6790=ORIENTED_EDGE ( 'NONE', *, *, #3503, .F. ) ;
#6792=B_SPLINE_CURVE_WITH_KNOTS ( 'NONE', 3,
 ( #1892, #5370, #5418, #133, #179, #4261, #5456, #1760, #4102, #2610, #4874, #6773, #4593, #5058, #1520, #5713, #2719, #2861 ),
 .UNSPECIFIED., .F., .F.,
 ( 4, 2, 2, 2, 2, 2, 2, 2, 4 ),
 ( -8.042425861386104689E-06, 0.0009212656149223902389, 0.001385919635314278395, 0.001850573655706166552, 0.002315227676098054709, 0.002779881696489942648, 0.003244535716881830588, 0.003476862727077775425, 0.003709189737273719829 ),
 .UNSPECIFIED. ) ;
#6803=FACE_OUTER_BOUND ( 'NONE', #688, .T. ) ;
#6804=CARTESIAN_POINT ( 'NONE',  ( -1.950024051643512521E-29, 1.861696953619914682E-15, -1.361499588670820771 ) ) ;
#6814=CARTESIAN_POINT ( 'NONE',  ( 0.9609181420092280934, 0.5141614760841562992, -1.361499588670821659 ) ) ;
#6817=ORIENTED_EDGE ( 'NONE', *, *, #5672, .T. ) ;
#6818=TOROIDAL_SURFACE ( 'NONE', #3891, 1.223643328182682621, 0.05905511811023622659 ) ;
#6819=CARTESIAN_POINT ( 'NONE',  ( 0.000000000000000000, 0.000000000000000000, -1.515748031496062964 ) ) ;
#6821=DIRECTION ( 'NONE',  ( -1.000000000000000000, -3.491481338843133355E-15, 0.000000000000000000 ) ) ;
#6822=CARTESIAN_POINT ( 'NONE',  ( 0.4330708661417322913, -0.9604263920613176353, -1.456063616177414310 ) ) ;
#6826=VERTEX_POINT ( 'NONE', #2445 ) ;
#6832=DIRECTION ( 'NONE',  ( -1.000000000000000000, 0.000000000000000000, 0.000000000000000000 ) ) ;
#6835=DIRECTION ( 'NONE',  ( -3.491481338843133750E-15, 1.000000000000000000, 4.625929269271482167E-15 ) ) ;
#6838=CARTESIAN_POINT ( 'NONE',  ( 0.4338950423154144254, 1.037563309807724821, -1.574803149606299302 ) ) ;
#6843=ORIENTED_EDGE ( 'NONE', *, *, #2530, .F. ) ;
#6850=VERTEX_POINT ( 'NONE', #653 ) ;
#6853=DIRECTION ( 'NONE',  ( -0.000000000000000000, 1.000000000000000000, 0.000000000000000000 ) ) ;
#6855=( NAMED_UNIT ( * ) SI_UNIT ( $, .STERADIAN. ) SOLID_ANGLE_UNIT ( ) );
#6865=TOROIDAL_SURFACE ( 'NONE', #4428, 1.223643328182681289, 0.05905511811023622659 ) ;
#6874=CIRCLE ( 'NONE', #4556, 1.089828288828796676 ) ;
#6880=ADVANCED_FACE ( 'NONE', ( #3593 ), #5155, .T. ) ;
#6883=AXIS2_PLACEMENT_3D ( 'NONE', #1091, #1595, #2783 ) ;
#6888=CARTESIAN_POINT ( 'NONE',  ( -0.9921522615226823216, -0.4406689276647633435, -1.439080857166196159 ) ) ;
#6890=DIRECTION ( 'NONE',  ( 7.708596820178695308E-30, -2.207829878515936732E-15, 1.000000000000000000 ) ) ;
#6892=VERTEX_POINT ( 'NONE', #7114 ) ;
#6901=ORIENTED_EDGE ( 'NONE', *, *, #5240, .F. ) ;
#6905=DIRECTION ( 'NONE',  ( 0.000000000000000000, 0.000000000000000000, -1.000000000000000000 ) ) ;
#6912=CARTESIAN_POINT ( 'NONE',  ( 0.4330708661417322913, -0.9666437042230126009, -1.454455828411335583 ) ) ;
#6913=EDGE_CURVE ( 'NONE', #3650, #5491, #515, .T. ) ;
#6914=EDGE_CURVE ( 'NONE', #2290, #5274, #7200, .T. ) ;
#6918=CARTESIAN_POINT ( 'NONE',  ( -0.4330708661417322913, -0.9666437042230143772, -1.454455828411337359 ) ) ;
#6920=DIMENSIONAL_EXPONENTS ( 1.000000000000000000, 0.000000000000000000, 0.000000000000000000, 0.000000000000000000, 0.000000000000000000, 0.000000000000000000, 0.000000000000000000 ) ;
#6924=ORIENTED_EDGE ( 'NONE', *, *, #4447, .F. ) ;
#6931=ORIENTED_EDGE ( 'NONE', *, *, #6733, .T. ) ;
#6939=AXIS2_PLACEMENT_3D ( 'NONE', #7370, #1094, #3946 ) ;
#6942=AXIS2_PLACEMENT_3D ( 'NONE', #6324, #7421, #3548 ) ;
#6946=CARTESIAN_POINT ( 'NONE',  ( -0.2362204724409449341, 2.892866454678787531E-17, 0.000000000000000000 ) ) ;
#6947=CARTESIAN_POINT ( 'NONE',  ( 0.4338950423154144254, -1.037563309807725043, -1.574803149606299302 ) ) ;
#6948=FACE_OUTER_BOUND ( 'NONE', #5496, .T. ) ;
#6950=DIRECTION ( 'NONE',  ( 1.000000000000000000, 0.000000000000000000, 0.000000000000000000 ) ) ;
#6952=CARTESIAN_POINT ( 'NONE',  ( -0.4475999628372195338, -0.9971723906835435747, -1.429777239771659048 ) ) ;
#6964=CARTESIAN_POINT ( 'NONE',  ( -0.5141614760841420884, 0.000000000000000000, -2.204724409448823419 ) ) ;
#6965=EDGE_CURVE ( 'NONE', #4341, #408, #3200, .T. ) ;
#6969=ORIENTED_EDGE ( 'NONE', *, *, #2615, .F. ) ;
#6970=ADVANCED_FACE ( 'NONE', ( #2958 ), #5262, .T. ) ;
#6977=CARTESIAN_POINT ( 'NONE',  ( -0.4330708661417315142, 1.044891351410290214, -1.574550377471545470 ) ) ;
#6986=CARTESIAN_POINT ( 'NONE',  ( 0.000000000000000000, 0.000000000000000000, -0.7983802283864783744 ) ) ;
#6989=ORIENTED_EDGE ( 'NONE', *, *, #5272, .T. ) ;
#6996=CARTESIAN_POINT ( 'NONE',  ( 0.000000000000000000, 0.000000000000000000, -1.546597720061111847 ) ) ;
#6998=EDGE_LOOP ( 'NONE', ( #4379, #2896, #3876, #5858 ) ) ;
#6999=CARTESIAN_POINT ( 'NONE',  ( 0.4882980771758823058, 0.9867934559254213367, -1.385219299502220336 ) ) ;
#7000=CARTESIAN_POINT ( 'NONE',  ( -0.9755734897585901511, 0.4619485889667589995, -1.553989674004691901 ) ) ;
#7001=VERTEX_POINT ( 'NONE', #5299 ) ;
#7009=ORIENTED_EDGE ( 'NONE', *, *, #5230, .T. ) ;
#7011=CARTESIAN_POINT ( 'NONE',  ( -0.4388997119412543779, -0.9346848099469042825, -1.455943619906243436 ) ) ;
#7014=EDGE_CURVE ( 'NONE', #135, #3031, #2287, .T. ) ;
#7018=FACE_OUTER_BOUND ( 'NONE', #4907, .T. ) ;
#7020=CARTESIAN_POINT ( 'NONE',  ( -0.9609181420092336445, 0.5141614760841427545, -1.361499588670819216 ) ) ;
#7026=DIRECTION ( 'NONE',  ( -0.000000000000000000, -0.000000000000000000, 1.000000000000000000 ) ) ;
#7027=CARTESIAN_POINT ( 'NONE',  ( 0.000000000000000000, 0.000000000000000000, -1.574803149606299302 ) ) ;
#7028=VERTEX_POINT ( 'NONE', #7292 ) ;
#7033=ORIENTED_EDGE ( 'NONE', *, *, #2666, .F. ) ;
#7034=FACE_OUTER_BOUND ( 'NONE', #5526, .T. ) ;
#7036=CARTESIAN_POINT ( 'NONE',  ( -0.9861598787149308265, 0.4544645342395042809, -1.560495034967182004 ) ) ;
#7041=CARTESIAN_POINT ( 'NONE',  ( 0.9964144355006142595, 2.543737003400971975E-44, -1.433776001880364026 ) ) ;
#7046=CARTESIAN_POINT ( 'NONE',  ( 6.221505307624544299E-30, -1.781909941321919274E-15, -1.397637795275591843 ) ) ;
#7047=CARTESIAN_POINT ( 'NONE',  ( -1.023372273685338785, -0.4368378848980560281, -1.573834172653142627 ) ) ;
#7052=CARTESIAN_POINT ( 'NONE',  ( -0.4559215864680341013, 0.8989373009621118849, -1.445239633971736604 ) ) ;
#7058=EDGE_CURVE ( 'NONE', #2045, #3366, #7459, .T. ) ;
#7060=DIRECTION ( 'NONE',  ( 3.491481338843133750E-15, -1.000000000000000000, -4.625929269271482167E-15 ) ) ;
#7063=CARTESIAN_POINT ( 'NONE',  ( -5.385555596699467400E-15, 0.5141614760841421994, -2.204724409448823419 ) ) ;
#7074=DIRECTION ( 'NONE',  ( 0.000000000000000000, 0.000000000000000000, 1.000000000000000000 ) ) ;
#7077=CARTESIAN_POINT ( 'NONE',  ( 0.4406690496059742501, 0.9921524035015029108, -1.439080679658372608 ) ) ;
#7081=CARTESIAN_POINT ( 'NONE',  ( 0.4353079511162236126, -0.9479499796399308842, -1.456692913385826849 ) ) ;
#7086=CARTESIAN_POINT ( 'NONE',  ( -1.063161251382697792, -0.4348450093584693699, -1.569784523562343770 ) ) ;
#7093=CARTESIAN_POINT ( 'NONE',  ( -1.084813395429189642, 0.4713813068963866870, -1.526966363676886873 ) ) ;
#7100=CARTESIAN_POINT ( 'NONE',  ( 0.4388997119412543779, -0.9346848099469029503, -1.455943619906241215 ) ) ;
#7105=ADVANCED_FACE ( 'NONE', ( #1405 ), #6622, .T. ) ;
#7106=CARTESIAN_POINT ( 'NONE',  ( 1.083679028610375239, 0.4756000659978086298, -1.522578585053779410 ) ) ;
#7114=CARTESIAN_POINT ( 'NONE',  ( 0.9479499796399277756, 0.4353079511162336046, -1.456692913385828625 ) ) ;
#7119=EDGE_LOOP ( 'NONE', ( #6439, #5513, #6924, #4802, #7224, #82 ) ) ;
#7120=DIRECTION ( 'NONE',  ( 5.296894631669315808E-46, -1.000000000000000000, 2.207829878515936732E-15 ) ) ;
#7141=CARTESIAN_POINT ( 'NONE',  ( -4.536176542591435797E-15, 0.4330708661417287941, -2.204724409448822975 ) ) ;
#7145=ORIENTED_EDGE ( 'NONE', *, *, #2615, .T. ) ;
#7148=CARTESIAN_POINT ( 'NONE',  ( 0.4341579107162097384, 1.060348520640340686, -1.570964845243103758 ) ) ;
#7155=ORIENTED_EDGE ( 'NONE', *, *, #6556, .T. ) ;
#7161=CARTESIAN_POINT ( 'NONE',  ( -1.075169953371341913, -0.4403524516314022974, -1.561970681382795823 ) ) ;
#7168=CARTESIAN_POINT ( 'NONE',  ( 0.4921259842519683514, 0.000000000000000000, -2.204724409448820754 ) ) ;
#7170=CARTESIAN_POINT ( 'NONE',  ( 1.060348520640336467, 0.4341579107162202300, -1.570964845243103314 ) ) ;
#7173=CARTESIAN_POINT ( 'NONE',  ( -1.866451592287363150E-29, 1.781909941321919274E-15, -1.397637795275591843 ) ) ;
#7178=CARTESIAN_POINT ( 'NONE',  ( -0.4330708661417317362, 1.048552902599920733, -1.573978973432617279 ) ) ;
#7179=AXIS2_PLACEMENT_3D ( 'NONE', #1073, #3417, #648 ) ;
#7191=EDGE_CURVE ( 'NONE', #5146, #383, #2465, .T. ) ;
#7200=B_SPLINE_CURVE_WITH_KNOTS ( 'NONE', 3,
 ( #1367, #7217, #841, #7257, #4933, #2595, #876, #4324, #4852, #3749, #272, #6658, #6054, #4357, #1991, #5555, #1402, #7178 ),
 .UNSPECIFIED., .F., .F.,
 ( 4, 2, 2, 2, 2, 2, 2, 2, 4 ),
 ( -8.042425861385237327E-06, 0.0009212656149223862273, 0.001385919635314276878, 0.001850573655706167636, 0.002315227676098058178, 0.002779881696489948720, 0.003244535716881839262, 0.003476862727077780196, 0.003709189737273721130 ),
 .UNSPECIFIED. ) ;
#7209=CARTESIAN_POINT ( 'NONE',  ( 1.085572762089306531, 0.4589126309195485365, -1.540322683979783447 ) ) ;
#7217=CARTESIAN_POINT ( 'NONE',  ( -0.5072158114897864500, 1.064252964791886580, -1.491281854711272059 ) ) ;
#7223=CARTESIAN_POINT ( 'NONE',  ( 0.4353079511162236126, 0.9479499796399308842, -1.456692913385826849 ) ) ;
#7224=ORIENTED_EDGE ( 'NONE', *, *, #2116, .T. ) ;
#7227=B_SPLINE_CURVE_WITH_KNOTS ( 'NONE', 3,
 ( #4643, #1226, #6977, #5159 ),
 .UNSPECIFIED., .F., .F.,
 ( 4, 4 ),
 ( 6.648767611728002819E-17, 0.0002807012396508846487 ),
 .UNSPECIFIED. ) ;
#7229=EDGE_CURVE ( 'NONE', #4054, #3405, #5400, .T. ) ;
#7235=ORIENTED_EDGE ( 'NONE', *, *, #2941, .F. ) ;
#7237=VERTEX_POINT ( 'NONE', #1705 ) ;
#7241=EDGE_CURVE ( 'NONE', #1329, #3366, #2931, .T. ) ;
#7249=CARTESIAN_POINT ( 'NONE',  ( 0.4878045971889972132, -1.078368813366570533, -1.510181706589752482 ) ) ;
#7252=CARTESIAN_POINT ( 'NONE',  ( 0.4700904924197906176, 0.8785537298370117432, -1.433776001880362250 ) ) ;
#7255=AXIS2_PLACEMENT_3D ( 'NONE', #6429, #2944, #6470 ) ;
#7256=DIRECTION ( 'NONE',  ( -1.000000000000000000, 0.000000000000000000, -2.256009703088257329E-15 ) ) ;
#7257=CARTESIAN_POINT ( 'NONE',  ( -0.4878048847236817753, 1.078368654584403563, -1.510181419419387661 ) ) ;
#7261=CARTESIAN_POINT ( 'NONE',  ( 0.5141614760841458631, 1.056523642887403192, -1.484898342931014303 ) ) ;
#7265=ORIENTED_EDGE ( 'NONE', *, *, #5850, .T. ) ;
#7268=CARTESIAN_POINT ( 'NONE',  ( 0.9867934559254264437, -0.4882980771758718697, -1.385219299502220114 ) ) ;
#7270=CARTESIAN_POINT ( 'NONE',  ( 0.9479499796399352141, -0.4353079511162137316, -1.456692913385826849 ) ) ;
#7274=ORIENTED_EDGE ( 'NONE', *, *, #4303, .T. ) ;
#7279=EDGE_CURVE ( 'NONE', #75, #3292, #6212, .T. ) ;
#7280=CARTESIAN_POINT ( 'NONE',  ( -0.8884022185686297757, -0.4627504720074800404, -1.439912370850676027 ) ) ;
#7281=CARTESIAN_POINT ( 'NONE',  ( -0.9666437042230142662, 0.4330708661417289052, -1.454455828411335583 ) ) ;
#7284=CARTESIAN_POINT ( 'NONE',  ( 1.044891351410292435, -0.4330708661417213556, -1.574550377471545692 ) ) ;
#7285=EDGE_CURVE ( 'NONE', #5278, #709, #2323, .T. ) ;
#7292=CARTESIAN_POINT ( 'NONE',  ( -1.089828288828796898, 1.213184216936748681E-31, -1.361499588670820771 ) ) ;
#7295=CARTESIAN_POINT ( 'NONE',  ( 0.4713815370807412641, 1.084813347358863478, -1.526966122205014820 ) ) ;
#7296=VERTEX_POINT ( 'NONE', #6495 ) ;
#7297=DIRECTION ( 'NONE',  ( -1.000000000000000000, -0.000000000000000000, 0.000000000000000000 ) ) ;
#7299=ORIENTED_EDGE ( 'NONE', *, *, #5844, .T. ) ;
#7301=CARTESIAN_POINT ( 'NONE',  ( 0.9941396836775437951, 0.4762527114670134232, -1.397361282224859780 ) ) ;
#7303=AXIS2_PLACEMENT_3D ( 'NONE', #7063, #4814, #5041 ) ;
#7305=B_SPLINE_CURVE_WITH_KNOTS ( 'NONE', 3,
 ( #2244, #557, #1660, #1583 ),
 .UNSPECIFIED., .F., .F.,
 ( 4, 4 ),
 ( 0.000000000000000000, 0.0004815725036528575279 ),
 .UNSPECIFIED. ) ;
#7316=AXIS2_PLACEMENT_3D ( 'NONE', #495, #5221, #6832 ) ;
#7318=B_SPLINE_CURVE_WITH_KNOTS ( 'NONE', 3,
 ( #5919, #6485, #4191, #3578 ),
 .UNSPECIFIED., .F., .F.,
 ( 4, 4 ),
 ( 6.648767611728001586E-17, 0.0002807012396508843776 ),
 .UNSPECIFIED. ) ;
#7324=CARTESIAN_POINT ( 'NONE',  ( 1.010073413237861928, 0.4416276115803188240, -1.570717210673253428 ) ) ;
#7327=ORIENTED_EDGE ( 'NONE', *, *, #4347, .T. ) ;
#7330=EDGE_CURVE ( 'NONE', #2214, #2732, #1600, .T. ) ;
#7331=DIRECTION ( 'NONE',  ( -1.224646799147353207E-16, 1.000000000000000000, 0.000000000000000000 ) ) ;
#7332=EDGE_CURVE ( 'NONE', #1484, #4949, #993, .T. ) ;
#7344=( GEOMETRIC_REPRESENTATION_CONTEXT ( 3 ) GLOBAL_UNCERTAINTY_ASSIGNED_CONTEXT ( ( #3583 ) ) GLOBAL_UNIT_ASSIGNED_CONTEXT ( ( #4188, #675, #6404 ) ) REPRESENTATION_CONTEXT ( 'NONE', 'WORKASPACE' ) );
#7350=ORIENTED_EDGE ( 'NONE', *, *, #7241, .F. ) ;
#7353=AXIS2_PLACEMENT_3D ( 'NONE', #3580, #3433, #102 ) ;
#7358=AXIS2_PLACEMENT_3D ( 'NONE', #3478, #5815, #1744 ) ;
#7366=ORIENTED_EDGE ( 'NONE', *, *, #4303, .F. ) ;
#7370=CARTESIAN_POINT ( 'NONE',  ( 0.5141614760841457521, 0.000000000000000000, -2.204724409448820754 ) ) ;
#7371=ORIENTED_EDGE ( 'NONE', *, *, #2989, .T. ) ;
#7385=CARTESIAN_POINT ( 'NONE',  ( 0.9479499796399277756, 0.4353079511162336046, -1.456692913385828625 ) ) ;
#7395=CARTESIAN_POINT ( 'NONE',  ( 0.9346850374427910779, 0.4388996395293667807, -1.455943645409048637 ) ) ;
#7397=FACE_OUTER_BOUND ( 'NONE', #2889, .T. ) ;
#7402=CARTESIAN_POINT ( 'NONE',  ( -0.4663806185492885836, -0.8833138556570210298, -1.436938405272246921 ) ) ;
#7403=CARTESIAN_POINT ( 'NONE',  ( -0.4700904924197902846, 0.9659644734970543878, -1.546597720061111847 ) ) ;
#7410=ORIENTED_EDGE ( 'NONE', *, *, #5791, .F. ) ;
#7413=EDGE_LOOP ( 'NONE', ( #7155, #5329, #6687, #6969, #6931, #7327, #514, #172, #2448, #519, #3835, #7299 ) ) ;
#7416=CARTESIAN_POINT ( 'NONE',  ( -1.718248690375557255E-15, 0.4921259842519683514, -2.204724409448820754 ) ) ;
#7417=CARTESIAN_POINT ( 'NONE',  ( -1.781909941321919274E-15, 0.000000000000000000, -1.397637795275591843 ) ) ;
#7418=EDGE_CURVE ( 'NONE', #6357, #1871, #5701, .T. ) ;
#7419=DIRECTION ( 'NONE',  ( 1.224646799147353207E-16, 1.000000000000000000, 0.000000000000000000 ) ) ;
#7421=DIRECTION ( 'NONE',  ( 1.000000000000000000, 0.000000000000000000, -0.000000000000000000 ) ) ;
#7423=AXIS2_PLACEMENT_3D ( 'NONE', #928, #6785, #4986 ) ;
#7426=ORIENTED_EDGE ( 'NONE', *, *, #6306, .F. ) ;
#7430=CARTESIAN_POINT ( 'NONE',  ( 0.8884031170519930409, 0.4627498550472279870, -1.439912866901233990 ) ) ;
#7433=AXIS2_PLACEMENT_3D ( 'NONE', #4320, #6653, #3744 ) ;
#7435=DIRECTION ( 'NONE',  ( -1.000000000000000000, 0.000000000000000000, 0.000000000000000000 ) ) ;
#7443=CARTESIAN_POINT ( 'NONE',  ( 0.4349192646538860285, -0.9810555383103363170, -1.448591292758282023 ) ) ;
#7459=CIRCLE ( 'NONE', #2580, 0.05905511811023620578 ) ;
#7460=DIRECTION ( 'NONE',  ( -1.000000000000000000, -0.000000000000000000, 0.000000000000000000 ) ) ;
#7461=EDGE_CURVE ( 'NONE', #283, #269, #4782, .T. ) ;
#7462=VERTEX_POINT ( 'NONE', #7281 ) ;
#7468=AXIS2_PLACEMENT_3D ( 'NONE', #551, #7460, #1616 ) ;
#7474=CARTESIAN_POINT ( 'NONE',  ( 0.9221073153504563136, -0.4437903857718229483, -1.453484209829403850 ) ) ;
#7476=CARTESIAN_POINT ( 'NONE',  ( -0.4921259842519648542, 0.000000000000000000, -2.204724409448822975 ) ) ;
#7484=CARTESIAN_POINT ( 'NONE',  ( -0.9941399105654876722, -0.4762522394722520369, -1.397361772547374814 ) ) ;
#7489=ORIENTED_EDGE ( 'NONE', *, *, #6396, .T. ) ;
#7493=ORIENTED_EDGE ( 'NONE', *, *, #4497, .T. ) ;
#7504=( LENGTH_UNIT ( ) NAMED_UNIT ( * ) SI_UNIT ( $, .METRE. ) );
#7508=DIRECTION ( 'NONE',  ( 0.000000000000000000, 0.000000000000000000, -1.000000000000000000 ) ) ;
#7510=CARTESIAN_POINT ( 'NONE',  ( -0.9159932075028757170, 0.4466261709646344169, -1.451746187131333521 ) ) ;
#7513=EDGE_CURVE ( 'NONE', #5534, #4463, #146, .T. ) ;
#7518=EDGE_CURVE ( 'NONE', #1871, #630, #3311, .T. ) ;
#7560=COLOUR_RGB('Light Blue',0.38,0.62,0.78);
#7561=FILL_AREA_STYLE_COLOUR('',#7560);
#7562=FILL_AREA_STYLE('',(#7561));
#7563=SURFACE_STYLE_FILL_AREA(#7562);
#7564=SURFACE_SIDE_STYLE('',(#7563));
#7565=SURFACE_STYLE_USAGE(.BOTH.,#7564);
#7566=PRESENTATION_STYLE_ASSIGNMENT((#7565));
ENDSEC;
END-ISO-10303-21;
